ISO-10303-21;
HEADER;
/* Generated by software containing ST-Developer
 * from STEP Tools, Inc. (www.steptools.com) 
 */

FILE_DESCRIPTION(
/* description */ ('STEP AP214'),
/* implementation_level */ '2;1');

FILE_NAME(
/* name */ 'PUR-HW-4061.step',
/* time_stamp */ '2026-10-07T12:49:37-07:00',
/* author */ (''),
/* organization */ (''),
/* preprocessor_version */ 'ST-DEVELOPER v20.2',
/* originating_system */ 'Autodesk Translation Framework v15.15.0.0',
/* authorisation */ '');

FILE_SCHEMA (('AUTOMOTIVE_DESIGN { 1 0 10303 214 3 1 1 }'));
ENDSEC;

DATA;
#10=MECHANICAL_DESIGN_GEOMETRIC_PRESENTATION_REPRESENTATION('',(#312),#33016);
#203=(
BOUNDED_CURVE()
B_SPLINE_CURVE(2,(#31599,#31600,#31601,#31602,#31603,#31604,#31605,#31606,
#31607,#31608,#31609,#31610,#31611,#31612,#31613,#31614,#31615),
 .UNSPECIFIED.,.F.,.F.)
B_SPLINE_CURVE_WITH_KNOTS((3,2,2,2,2,2,2,2,3),(0.75,0.78125,0.8125,0.84375,
0.875,0.90625,0.9375,0.96875,1.),.UNSPECIFIED.)
CURVE()
GEOMETRIC_REPRESENTATION_ITEM()
RATIONAL_B_SPLINE_CURVE((1.,0.923879532511287,1.,0.923879532511287,1.,0.923879532511287,
1.,0.923879532511287,1.,0.923879532511287,1.,0.923879532511287,1.,0.923879532511287,
1.,0.923879532511287,1.))
REPRESENTATION_ITEM('')
);
#204=(
BOUNDED_CURVE()
B_SPLINE_CURVE(2,(#31617,#31618,#31619,#31620,#31621,#31622,#31623,#31624,
#31625,#31626,#31627,#31628,#31629,#31630,#31631,#31632,#31633,#31634,#31635,
#31636,#31637,#31638,#31639,#31640,#31641,#31642,#31643,#31644,#31645,#31646,
#31647,#31648,#31649,#31650,#31651,#31652,#31653,#31654,#31655,#31656,#31657,
#31658,#31659,#31660,#31661,#31662,#31663,#31664,#31665),.UNSPECIFIED.,
 .F.,.F.)
B_SPLINE_CURVE_WITH_KNOTS((3,2,2,2,2,2,2,2,2,2,2,2,2,2,2,2,2,2,2,2,2,2,
2,2,3),(0.,0.03125,0.0625,0.09375,0.125,0.15625,0.1875,0.21875,0.25,0.28125,
0.3125,0.34375,0.375,0.40625,0.4375,0.46875,0.5,0.53125,0.5625,0.59375,
0.625,0.65625,0.6875,0.71875,0.75),.UNSPECIFIED.)
CURVE()
GEOMETRIC_REPRESENTATION_ITEM()
RATIONAL_B_SPLINE_CURVE((1.,0.923879532511287,1.,0.923879532511287,1.,0.923879532511287,
1.,0.923879532511287,1.,0.923879532511287,1.,0.923879532511287,1.,0.923879532511287,
1.,0.923879532511287,1.,0.923879532511287,1.,0.923879532511287,1.,0.923879532511287,
1.,0.923879532511287,1.,0.923879532511287,1.,0.923879532511287,1.,0.923879532511287,
1.,0.923879532511287,1.,0.923879532511287,1.,0.923879532511287,1.,0.923879532511287,
1.,0.923879532511287,1.,0.923879532511287,1.,0.923879532511287,1.,0.923879532511287,
1.,0.923879532511287,1.))
REPRESENTATION_ITEM('')
);
#205=(
BOUNDED_CURVE()
B_SPLINE_CURVE(2,(#31668,#31669,#31670,#31671,#31672,#31673,#31674,#31675,
#31676,#31677,#31678,#31679,#31680,#31681,#31682,#31683,#31684,#31685,#31686,
#31687,#31688,#31689,#31690,#31691,#31692,#31693,#31694,#31695,#31696,#31697,
#31698,#31699,#31700,#31701,#31702,#31703,#31704,#31705,#31706,#31707,#31708,
#31709,#31710,#31711,#31712,#31713,#31714,#31715,#31716,#31717,#31718,#31719,
#31720,#31721,#31722,#31723,#31724,#31725,#31726,#31727,#31728,#31729,#31730,
#31731,#31732),.UNSPECIFIED.,.F.,.F.)
B_SPLINE_CURVE_WITH_KNOTS((3,2,2,2,2,2,2,2,2,2,2,2,2,2,2,2,2,2,2,2,2,2,
2,2,2,2,2,2,2,2,2,2,3),(0.,0.03125,0.0625,0.09375,0.125,0.15625,0.1875,
0.21875,0.25,0.28125,0.3125,0.34375,0.375,0.40625,0.4375,0.46875,0.5,0.53125,
0.5625,0.59375,0.625,0.65625,0.6875,0.71875,0.75,0.78125,0.8125,0.84375,
0.875,0.90625,0.9375,0.96875,1.),.UNSPECIFIED.)
CURVE()
GEOMETRIC_REPRESENTATION_ITEM()
RATIONAL_B_SPLINE_CURVE((1.,0.923879532511287,1.,0.923879532511287,1.,0.923879532511287,
1.,0.923879532511287,1.,0.923879532511287,1.,0.923879532511287,1.,0.923879532511287,
1.,0.923879532511287,1.,0.923879532511287,1.,0.923879532511287,1.,0.923879532511287,
1.,0.923879532511287,1.,0.923879532511287,1.,0.923879532511287,1.,0.923879532511287,
1.,0.923879532511287,1.,0.923879532511287,1.,0.923879532511287,1.,0.923879532511287,
1.,0.923879532511287,1.,0.923879532511287,1.,0.923879532511287,1.,0.923879532511287,
1.,0.923879532511287,1.,0.923879532511287,1.,0.923879532511287,1.,0.923879532511287,
1.,0.923879532511287,1.,0.923879532511287,1.,0.923879532511287,1.,0.923879532511287,
1.,0.923879532511287,1.))
REPRESENTATION_ITEM('')
);
#206=(
BOUNDED_CURVE()
B_SPLINE_CURVE(2,(#31995,#31996,#31997,#31998,#31999,#32000,#32001,#32002,
#32003,#32004,#32005,#32006,#32007,#32008,#32009,#32010,#32011),
 .UNSPECIFIED.,.F.,.F.)
B_SPLINE_CURVE_WITH_KNOTS((3,2,2,2,2,2,2,2,3),(0.,0.03125,0.0625,0.09375,
0.125,0.15625,0.1875,0.21875,0.25),.UNSPECIFIED.)
CURVE()
GEOMETRIC_REPRESENTATION_ITEM()
RATIONAL_B_SPLINE_CURVE((1.,0.923879532511287,1.,0.923879532511287,1.,0.923879532511287,
1.,0.923879532511287,1.,0.923879532511287,1.,0.923879532511287,1.,0.923879532511287,
1.,0.923879532511287,1.))
REPRESENTATION_ITEM('')
);
#207=(
BOUNDED_CURVE()
B_SPLINE_CURVE(2,(#32012,#32013,#32014,#32015,#32016,#32017,#32018,#32019,
#32020,#32021,#32022,#32023,#32024,#32025,#32026,#32027,#32028,#32029,#32030,
#32031,#32032,#32033,#32034,#32035,#32036,#32037,#32038,#32039,#32040,#32041,
#32042,#32043,#32044,#32045,#32046,#32047,#32048,#32049,#32050,#32051,#32052,
#32053,#32054,#32055,#32056,#32057,#32058,#32059,#32060),.UNSPECIFIED.,
 .F.,.F.)
B_SPLINE_CURVE_WITH_KNOTS((3,2,2,2,2,2,2,2,2,2,2,2,2,2,2,2,2,2,2,2,2,2,
2,2,3),(0.,0.03125,0.0625,0.09375,0.125,0.15625,0.1875,0.21875,0.25,0.28125,
0.3125,0.34375,0.375,0.40625,0.4375,0.46875,0.5,0.53125,0.5625,0.59375,
0.625,0.65625,0.6875,0.71875,0.75),.UNSPECIFIED.)
CURVE()
GEOMETRIC_REPRESENTATION_ITEM()
RATIONAL_B_SPLINE_CURVE((1.,0.923879532511287,1.,0.923879532511287,1.,0.923879532511287,
1.,0.923879532511287,1.,0.923879532511287,1.,0.923879532511287,1.,0.923879532511287,
1.,0.923879532511287,1.,0.923879532511287,1.,0.923879532511287,1.,0.923879532511287,
1.,0.923879532511287,1.,0.923879532511287,1.,0.923879532511287,1.,0.923879532511287,
1.,0.923879532511287,1.,0.923879532511287,1.,0.923879532511287,1.,0.923879532511287,
1.,0.923879532511287,1.,0.923879532511287,1.,0.923879532511287,1.,0.923879532511287,
1.,0.923879532511287,1.))
REPRESENTATION_ITEM('')
);
#208=(
BOUNDED_CURVE()
B_SPLINE_CURVE(2,(#32325,#32326,#32327,#32328,#32329,#32330,#32331,#32332,
#32333,#32334,#32335,#32336,#32337,#32338,#32339,#32340,#32341,#32342,#32343,
#32344,#32345,#32346,#32347,#32348,#32349,#32350,#32351,#32352,#32353,#32354,
#32355,#32356,#32357,#32358,#32359,#32360,#32361,#32362,#32363,#32364,#32365,
#32366,#32367,#32368,#32369,#32370,#32371,#32372,#32373,#32374,#32375,#32376,
#32377,#32378,#32379,#32380,#32381,#32382,#32383,#32384,#32385,#32386,#32387,
#32388,#32389),.UNSPECIFIED.,.F.,.F.)
B_SPLINE_CURVE_WITH_KNOTS((3,2,2,2,2,2,2,2,2,2,2,2,2,2,2,2,2,2,2,2,2,2,
2,2,2,2,2,2,2,2,2,2,3),(0.,0.03125,0.0625,0.09375,0.125,0.15625,0.1875,
0.21875,0.25,0.28125,0.3125,0.34375,0.375,0.40625,0.4375,0.46875,0.5,0.53125,
0.5625,0.59375,0.625,0.65625,0.6875,0.71875,0.75,0.78125,0.8125,0.84375,
0.875,0.90625,0.9375,0.96875,1.),.UNSPECIFIED.)
CURVE()
GEOMETRIC_REPRESENTATION_ITEM()
RATIONAL_B_SPLINE_CURVE((1.,0.923879532511287,1.,0.923879532511287,1.,0.923879532511287,
1.,0.923879532511287,1.,0.923879532511287,1.,0.923879532511287,1.,0.923879532511287,
1.,0.923879532511287,1.,0.923879532511287,1.,0.923879532511287,1.,0.923879532511287,
1.,0.923879532511287,1.,0.923879532511287,1.,0.923879532511287,1.,0.923879532511287,
1.,0.923879532511287,1.,0.923879532511287,1.,0.923879532511287,1.,0.923879532511287,
1.,0.923879532511287,1.,0.923879532511287,1.,0.923879532511287,1.,0.923879532511287,
1.,0.923879532511287,1.,0.923879532511287,1.,0.923879532511287,1.,0.923879532511287,
1.,0.923879532511287,1.,0.923879532511287,1.,0.923879532511287,1.,0.923879532511287,
1.,0.923879532511287,1.))
REPRESENTATION_ITEM('')
);
#254=SHAPE_REPRESENTATION_RELATIONSHIP('SRR','None',#33149,#281);
#281=ADVANCED_BREP_SHAPE_REPRESENTATION('',(#339),#33010);
#312=STYLED_ITEM('',(#33285),#339);
#339=MANIFOLD_SOLID_BREP('Body1',#9963);
#470=(
BOUNDED_SURFACE()
B_SPLINE_SURFACE(3,2,((#31335,#31336,#31337,#31338,#31339,#31340,#31341,
#31342,#31343,#31344,#31345,#31346,#31347,#31348,#31349,#31350,#31351,#31352,
#31353,#31354,#31355,#31356,#31357,#31358,#31359,#31360,#31361,#31362,#31363,
#31364,#31365,#31366,#31367,#31368,#31369,#31370,#31371,#31372,#31373,#31374,
#31375,#31376,#31377,#31378,#31379,#31380,#31381,#31382,#31383,#31384,#31385,
#31386,#31387,#31388,#31389,#31390,#31391,#31392,#31393,#31394,#31395,#31396,
#31397,#31398,#31399),(#31400,#31401,#31402,#31403,#31404,#31405,#31406,
#31407,#31408,#31409,#31410,#31411,#31412,#31413,#31414,#31415,#31416,#31417,
#31418,#31419,#31420,#31421,#31422,#31423,#31424,#31425,#31426,#31427,#31428,
#31429,#31430,#31431,#31432,#31433,#31434,#31435,#31436,#31437,#31438,#31439,
#31440,#31441,#31442,#31443,#31444,#31445,#31446,#31447,#31448,#31449,#31450,
#31451,#31452,#31453,#31454,#31455,#31456,#31457,#31458,#31459,#31460,#31461,
#31462,#31463,#31464),(#31465,#31466,#31467,#31468,#31469,#31470,#31471,
#31472,#31473,#31474,#31475,#31476,#31477,#31478,#31479,#31480,#31481,#31482,
#31483,#31484,#31485,#31486,#31487,#31488,#31489,#31490,#31491,#31492,#31493,
#31494,#31495,#31496,#31497,#31498,#31499,#31500,#31501,#31502,#31503,#31504,
#31505,#31506,#31507,#31508,#31509,#31510,#31511,#31512,#31513,#31514,#31515,
#31516,#31517,#31518,#31519,#31520,#31521,#31522,#31523,#31524,#31525,#31526,
#31527,#31528,#31529),(#31530,#31531,#31532,#31533,#31534,#31535,#31536,
#31537,#31538,#31539,#31540,#31541,#31542,#31543,#31544,#31545,#31546,#31547,
#31548,#31549,#31550,#31551,#31552,#31553,#31554,#31555,#31556,#31557,#31558,
#31559,#31560,#31561,#31562,#31563,#31564,#31565,#31566,#31567,#31568,#31569,
#31570,#31571,#31572,#31573,#31574,#31575,#31576,#31577,#31578,#31579,#31580,
#31581,#31582,#31583,#31584,#31585,#31586,#31587,#31588,#31589,#31590,#31591,
#31592,#31593,#31594)),.UNSPECIFIED.,.F.,.F.,.F.)
B_SPLINE_SURFACE_WITH_KNOTS((4,4),(3,2,2,2,2,2,2,2,2,2,2,2,2,2,2,2,2,2,
2,2,2,2,2,2,2,2,2,2,2,2,2,2,3),(0.,1.),(0.,0.03125,0.0625,0.09375,0.125,
0.15625,0.1875,0.21875,0.25,0.28125,0.3125,0.34375,0.375,0.40625,0.4375,
0.46875,0.5,0.53125,0.5625,0.59375,0.625,0.65625,0.6875,0.71875,0.75,0.78125,
0.8125,0.84375,0.875,0.90625,0.9375,0.96875,1.),.UNSPECIFIED.)
GEOMETRIC_REPRESENTATION_ITEM()
RATIONAL_B_SPLINE_SURFACE(((1.,0.923879532511287,1.,0.923879532511287,1.,
0.923879532511287,1.,0.923879532511287,1.,0.923879532511287,1.,0.923879532511287,
1.,0.923879532511287,1.,0.923879532511287,1.,0.923879532511287,1.,0.923879532511287,
1.,0.923879532511287,1.,0.923879532511287,1.,0.923879532511287,1.,0.923879532511287,
1.,0.923879532511287,1.,0.923879532511287,1.,0.923879532511287,1.,0.923879532511287,
1.,0.923879532511287,1.,0.923879532511287,1.,0.923879532511287,1.,0.923879532511287,
1.,0.923879532511287,1.,0.923879532511287,1.,0.923879532511287,1.,0.923879532511287,
1.,0.923879532511287,1.,0.923879532511287,1.,0.923879532511287,1.,0.923879532511287,
1.,0.923879532511287,1.,0.923879532511287,1.),(0.804737854124365,0.743480832462554,
0.804737854124365,0.743480832462554,0.804737854124365,0.743480832462554,
0.804737854124365,0.743480832462554,0.804737854124365,0.743480832462554,
0.804737854124365,0.743480832462554,0.804737854124365,0.743480832462554,
0.804737854124365,0.743480832462554,0.804737854124365,0.743480832462554,
0.804737854124365,0.743480832462554,0.804737854124365,0.743480832462554,
0.804737854124365,0.743480832462554,0.804737854124365,0.743480832462554,
0.804737854124365,0.743480832462554,0.804737854124365,0.743480832462554,
0.804737854124365,0.743480832462554,0.804737854124365,0.743480832462554,
0.804737854124365,0.743480832462554,0.804737854124365,0.743480832462554,
0.804737854124365,0.743480832462554,0.804737854124365,0.743480832462554,
0.804737854124365,0.743480832462554,0.804737854124365,0.743480832462554,
0.804737854124365,0.743480832462554,0.804737854124365,0.743480832462554,
0.804737854124365,0.743480832462554,0.804737854124365,0.743480832462554,
0.804737854124365,0.743480832462554,0.804737854124365,0.743480832462554,
0.804737854124365,0.743480832462554,0.804737854124365,0.743480832462554,
0.804737854124365,0.743480832462554,0.804737854124365),(0.804737854124365,
0.743480832462554,0.804737854124365,0.743480832462554,0.804737854124365,
0.743480832462554,0.804737854124365,0.743480832462554,0.804737854124365,
0.743480832462554,0.804737854124365,0.743480832462554,0.804737854124365,
0.743480832462554,0.804737854124365,0.743480832462554,0.804737854124365,
0.743480832462554,0.804737854124365,0.743480832462554,0.804737854124365,
0.743480832462554,0.804737854124365,0.743480832462554,0.804737854124365,
0.743480832462554,0.804737854124365,0.743480832462554,0.804737854124365,
0.743480832462554,0.804737854124365,0.743480832462554,0.804737854124365,
0.743480832462554,0.804737854124365,0.743480832462554,0.804737854124365,
0.743480832462554,0.804737854124365,0.743480832462554,0.804737854124365,
0.743480832462554,0.804737854124365,0.743480832462554,0.804737854124365,
0.743480832462554,0.804737854124365,0.743480832462554,0.804737854124365,
0.743480832462554,0.804737854124365,0.743480832462554,0.804737854124365,
0.743480832462554,0.804737854124365,0.743480832462554,0.804737854124365,
0.743480832462554,0.804737854124365,0.743480832462554,0.804737854124365,
0.743480832462554,0.804737854124365,0.743480832462554,0.804737854124365),
(1.,0.923879532511287,1.,0.923879532511287,1.,0.923879532511287,1.,0.923879532511287,
1.,0.923879532511287,1.,0.923879532511287,1.,0.923879532511287,1.,0.923879532511287,
1.,0.923879532511287,1.,0.923879532511287,1.,0.923879532511287,1.,0.923879532511287,
1.,0.923879532511287,1.,0.923879532511287,1.,0.923879532511287,1.,0.923879532511287,
1.,0.923879532511287,1.,0.923879532511287,1.,0.923879532511287,1.,0.923879532511287,
1.,0.923879532511287,1.,0.923879532511287,1.,0.923879532511287,1.,0.923879532511287,
1.,0.923879532511287,1.,0.923879532511287,1.,0.923879532511287,1.,0.923879532511287,
1.,0.923879532511287,1.,0.923879532511287,1.,0.923879532511287,1.,0.923879532511287,
1.)))
REPRESENTATION_ITEM('')
SURFACE()
);
#471=(
BOUNDED_SURFACE()
B_SPLINE_SURFACE(3,2,((#31733,#31734,#31735,#31736,#31737,#31738,#31739,
#31740,#31741,#31742,#31743,#31744,#31745,#31746,#31747,#31748,#31749,#31750,
#31751,#31752,#31753,#31754,#31755,#31756,#31757,#31758,#31759,#31760,#31761,
#31762,#31763,#31764,#31765,#31766,#31767,#31768,#31769,#31770,#31771,#31772,
#31773,#31774,#31775,#31776,#31777,#31778,#31779,#31780,#31781,#31782,#31783,
#31784,#31785,#31786,#31787,#31788,#31789,#31790,#31791,#31792,#31793,#31794,
#31795,#31796,#31797),(#31798,#31799,#31800,#31801,#31802,#31803,#31804,
#31805,#31806,#31807,#31808,#31809,#31810,#31811,#31812,#31813,#31814,#31815,
#31816,#31817,#31818,#31819,#31820,#31821,#31822,#31823,#31824,#31825,#31826,
#31827,#31828,#31829,#31830,#31831,#31832,#31833,#31834,#31835,#31836,#31837,
#31838,#31839,#31840,#31841,#31842,#31843,#31844,#31845,#31846,#31847,#31848,
#31849,#31850,#31851,#31852,#31853,#31854,#31855,#31856,#31857,#31858,#31859,
#31860,#31861,#31862),(#31863,#31864,#31865,#31866,#31867,#31868,#31869,
#31870,#31871,#31872,#31873,#31874,#31875,#31876,#31877,#31878,#31879,#31880,
#31881,#31882,#31883,#31884,#31885,#31886,#31887,#31888,#31889,#31890,#31891,
#31892,#31893,#31894,#31895,#31896,#31897,#31898,#31899,#31900,#31901,#31902,
#31903,#31904,#31905,#31906,#31907,#31908,#31909,#31910,#31911,#31912,#31913,
#31914,#31915,#31916,#31917,#31918,#31919,#31920,#31921,#31922,#31923,#31924,
#31925,#31926,#31927),(#31928,#31929,#31930,#31931,#31932,#31933,#31934,
#31935,#31936,#31937,#31938,#31939,#31940,#31941,#31942,#31943,#31944,#31945,
#31946,#31947,#31948,#31949,#31950,#31951,#31952,#31953,#31954,#31955,#31956,
#31957,#31958,#31959,#31960,#31961,#31962,#31963,#31964,#31965,#31966,#31967,
#31968,#31969,#31970,#31971,#31972,#31973,#31974,#31975,#31976,#31977,#31978,
#31979,#31980,#31981,#31982,#31983,#31984,#31985,#31986,#31987,#31988,#31989,
#31990,#31991,#31992)),.UNSPECIFIED.,.F.,.F.,.F.)
B_SPLINE_SURFACE_WITH_KNOTS((4,4),(3,2,2,2,2,2,2,2,2,2,2,2,2,2,2,2,2,2,
2,2,2,2,2,2,2,2,2,2,2,2,2,2,3),(0.,1.),(0.,0.03125,0.0625,0.09375,0.125,
0.15625,0.1875,0.21875,0.25,0.28125,0.3125,0.34375,0.375,0.40625,0.4375,
0.46875,0.5,0.53125,0.5625,0.59375,0.625,0.65625,0.6875,0.71875,0.75,0.78125,
0.8125,0.84375,0.875,0.90625,0.9375,0.96875,1.),.UNSPECIFIED.)
GEOMETRIC_REPRESENTATION_ITEM()
RATIONAL_B_SPLINE_SURFACE(((1.,0.923879532511287,1.,0.923879532511287,1.,
0.923879532511287,1.,0.923879532511287,1.,0.923879532511287,1.,0.923879532511287,
1.,0.923879532511287,1.,0.923879532511287,1.,0.923879532511287,1.,0.923879532511287,
1.,0.923879532511287,1.,0.923879532511287,1.,0.923879532511287,1.,0.923879532511287,
1.,0.923879532511287,1.,0.923879532511287,1.,0.923879532511287,1.,0.923879532511287,
1.,0.923879532511287,1.,0.923879532511287,1.,0.923879532511287,1.,0.923879532511287,
1.,0.923879532511287,1.,0.923879532511287,1.,0.923879532511287,1.,0.923879532511287,
1.,0.923879532511287,1.,0.923879532511287,1.,0.923879532511287,1.,0.923879532511287,
1.,0.923879532511287,1.,0.923879532511287,1.),(0.804737854124365,0.743480832462554,
0.804737854124365,0.743480832462554,0.804737854124365,0.743480832462554,
0.804737854124365,0.743480832462554,0.804737854124365,0.743480832462554,
0.804737854124365,0.743480832462554,0.804737854124365,0.743480832462554,
0.804737854124365,0.743480832462554,0.804737854124365,0.743480832462554,
0.804737854124365,0.743480832462554,0.804737854124365,0.743480832462554,
0.804737854124365,0.743480832462554,0.804737854124365,0.743480832462554,
0.804737854124365,0.743480832462554,0.804737854124365,0.743480832462554,
0.804737854124365,0.743480832462554,0.804737854124365,0.743480832462554,
0.804737854124365,0.743480832462554,0.804737854124365,0.743480832462554,
0.804737854124365,0.743480832462554,0.804737854124365,0.743480832462554,
0.804737854124365,0.743480832462554,0.804737854124365,0.743480832462554,
0.804737854124365,0.743480832462554,0.804737854124365,0.743480832462554,
0.804737854124365,0.743480832462554,0.804737854124365,0.743480832462554,
0.804737854124365,0.743480832462554,0.804737854124365,0.743480832462554,
0.804737854124365,0.743480832462554,0.804737854124365,0.743480832462554,
0.804737854124365,0.743480832462554,0.804737854124365),(0.804737854124365,
0.743480832462554,0.804737854124365,0.743480832462554,0.804737854124365,
0.743480832462554,0.804737854124365,0.743480832462554,0.804737854124365,
0.743480832462554,0.804737854124365,0.743480832462554,0.804737854124365,
0.743480832462554,0.804737854124365,0.743480832462554,0.804737854124365,
0.743480832462554,0.804737854124365,0.743480832462554,0.804737854124365,
0.743480832462554,0.804737854124365,0.743480832462554,0.804737854124365,
0.743480832462554,0.804737854124365,0.743480832462554,0.804737854124365,
0.743480832462554,0.804737854124365,0.743480832462554,0.804737854124365,
0.743480832462554,0.804737854124365,0.743480832462554,0.804737854124365,
0.743480832462554,0.804737854124365,0.743480832462554,0.804737854124365,
0.743480832462554,0.804737854124365,0.743480832462554,0.804737854124365,
0.743480832462554,0.804737854124365,0.743480832462554,0.804737854124365,
0.743480832462554,0.804737854124365,0.743480832462554,0.804737854124365,
0.743480832462554,0.804737854124365,0.743480832462554,0.804737854124365,
0.743480832462554,0.804737854124365,0.743480832462554,0.804737854124365,
0.743480832462554,0.804737854124365,0.743480832462554,0.804737854124365),
(1.,0.923879532511287,1.,0.923879532511287,1.,0.923879532511287,1.,0.923879532511287,
1.,0.923879532511287,1.,0.923879532511287,1.,0.923879532511287,1.,0.923879532511287,
1.,0.923879532511287,1.,0.923879532511287,1.,0.923879532511287,1.,0.923879532511287,
1.,0.923879532511287,1.,0.923879532511287,1.,0.923879532511287,1.,0.923879532511287,
1.,0.923879532511287,1.,0.923879532511287,1.,0.923879532511287,1.,0.923879532511287,
1.,0.923879532511287,1.,0.923879532511287,1.,0.923879532511287,1.,0.923879532511287,
1.,0.923879532511287,1.,0.923879532511287,1.,0.923879532511287,1.,0.923879532511287,
1.,0.923879532511287,1.,0.923879532511287,1.,0.923879532511287,1.,0.923879532511287,
1.)))
REPRESENTATION_ITEM('')
SURFACE()
);
#472=(
BOUNDED_SURFACE()
B_SPLINE_SURFACE(3,2,((#32062,#32063,#32064,#32065,#32066,#32067,#32068,
#32069,#32070,#32071,#32072,#32073,#32074,#32075,#32076,#32077,#32078,#32079,
#32080,#32081,#32082,#32083,#32084,#32085,#32086,#32087,#32088,#32089,#32090,
#32091,#32092,#32093,#32094,#32095,#32096,#32097,#32098,#32099,#32100,#32101,
#32102,#32103,#32104,#32105,#32106,#32107,#32108,#32109,#32110,#32111,#32112,
#32113,#32114,#32115,#32116,#32117,#32118,#32119,#32120,#32121,#32122,#32123,
#32124,#32125,#32126),(#32127,#32128,#32129,#32130,#32131,#32132,#32133,
#32134,#32135,#32136,#32137,#32138,#32139,#32140,#32141,#32142,#32143,#32144,
#32145,#32146,#32147,#32148,#32149,#32150,#32151,#32152,#32153,#32154,#32155,
#32156,#32157,#32158,#32159,#32160,#32161,#32162,#32163,#32164,#32165,#32166,
#32167,#32168,#32169,#32170,#32171,#32172,#32173,#32174,#32175,#32176,#32177,
#32178,#32179,#32180,#32181,#32182,#32183,#32184,#32185,#32186,#32187,#32188,
#32189,#32190,#32191),(#32192,#32193,#32194,#32195,#32196,#32197,#32198,
#32199,#32200,#32201,#32202,#32203,#32204,#32205,#32206,#32207,#32208,#32209,
#32210,#32211,#32212,#32213,#32214,#32215,#32216,#32217,#32218,#32219,#32220,
#32221,#32222,#32223,#32224,#32225,#32226,#32227,#32228,#32229,#32230,#32231,
#32232,#32233,#32234,#32235,#32236,#32237,#32238,#32239,#32240,#32241,#32242,
#32243,#32244,#32245,#32246,#32247,#32248,#32249,#32250,#32251,#32252,#32253,
#32254,#32255,#32256),(#32257,#32258,#32259,#32260,#32261,#32262,#32263,
#32264,#32265,#32266,#32267,#32268,#32269,#32270,#32271,#32272,#32273,#32274,
#32275,#32276,#32277,#32278,#32279,#32280,#32281,#32282,#32283,#32284,#32285,
#32286,#32287,#32288,#32289,#32290,#32291,#32292,#32293,#32294,#32295,#32296,
#32297,#32298,#32299,#32300,#32301,#32302,#32303,#32304,#32305,#32306,#32307,
#32308,#32309,#32310,#32311,#32312,#32313,#32314,#32315,#32316,#32317,#32318,
#32319,#32320,#32321)),.UNSPECIFIED.,.F.,.F.,.F.)
B_SPLINE_SURFACE_WITH_KNOTS((4,4),(3,2,2,2,2,2,2,2,2,2,2,2,2,2,2,2,2,2,
2,2,2,2,2,2,2,2,2,2,2,2,2,2,3),(0.,1.),(0.,0.03125,0.0625,0.09375,0.125,
0.15625,0.1875,0.21875,0.25,0.28125,0.3125,0.34375,0.375,0.40625,0.4375,
0.46875,0.5,0.53125,0.5625,0.59375,0.625,0.65625,0.6875,0.71875,0.75,0.78125,
0.8125,0.84375,0.875,0.90625,0.9375,0.96875,1.),.UNSPECIFIED.)
GEOMETRIC_REPRESENTATION_ITEM()
RATIONAL_B_SPLINE_SURFACE(((1.,0.923879532511287,1.,0.923879532511287,1.,
0.923879532511287,1.,0.923879532511287,1.,0.923879532511287,1.,0.923879532511287,
1.,0.923879532511287,1.,0.923879532511287,1.,0.923879532511287,1.,0.923879532511287,
1.,0.923879532511287,1.,0.923879532511287,1.,0.923879532511287,1.,0.923879532511287,
1.,0.923879532511287,1.,0.923879532511287,1.,0.923879532511287,1.,0.923879532511287,
1.,0.923879532511287,1.,0.923879532511287,1.,0.923879532511287,1.,0.923879532511287,
1.,0.923879532511287,1.,0.923879532511287,1.,0.923879532511287,1.,0.923879532511287,
1.,0.923879532511287,1.,0.923879532511287,1.,0.923879532511287,1.,0.923879532511287,
1.,0.923879532511287,1.,0.923879532511287,1.),(0.804737854124365,0.743480832462554,
0.804737854124365,0.743480832462554,0.804737854124365,0.743480832462554,
0.804737854124365,0.743480832462554,0.804737854124365,0.743480832462554,
0.804737854124365,0.743480832462554,0.804737854124365,0.743480832462554,
0.804737854124365,0.743480832462554,0.804737854124365,0.743480832462554,
0.804737854124365,0.743480832462554,0.804737854124365,0.743480832462554,
0.804737854124365,0.743480832462554,0.804737854124365,0.743480832462554,
0.804737854124365,0.743480832462554,0.804737854124365,0.743480832462554,
0.804737854124365,0.743480832462554,0.804737854124365,0.743480832462554,
0.804737854124365,0.743480832462554,0.804737854124365,0.743480832462554,
0.804737854124365,0.743480832462554,0.804737854124365,0.743480832462554,
0.804737854124365,0.743480832462554,0.804737854124365,0.743480832462554,
0.804737854124365,0.743480832462554,0.804737854124365,0.743480832462554,
0.804737854124365,0.743480832462554,0.804737854124365,0.743480832462554,
0.804737854124365,0.743480832462554,0.804737854124365,0.743480832462554,
0.804737854124365,0.743480832462554,0.804737854124365,0.743480832462554,
0.804737854124365,0.743480832462554,0.804737854124365),(0.804737854124365,
0.743480832462554,0.804737854124365,0.743480832462554,0.804737854124365,
0.743480832462554,0.804737854124365,0.743480832462554,0.804737854124365,
0.743480832462554,0.804737854124365,0.743480832462554,0.804737854124365,
0.743480832462554,0.804737854124365,0.743480832462554,0.804737854124365,
0.743480832462554,0.804737854124365,0.743480832462554,0.804737854124365,
0.743480832462554,0.804737854124365,0.743480832462554,0.804737854124365,
0.743480832462554,0.804737854124365,0.743480832462554,0.804737854124365,
0.743480832462554,0.804737854124365,0.743480832462554,0.804737854124365,
0.743480832462554,0.804737854124365,0.743480832462554,0.804737854124365,
0.743480832462554,0.804737854124365,0.743480832462554,0.804737854124365,
0.743480832462554,0.804737854124365,0.743480832462554,0.804737854124365,
0.743480832462554,0.804737854124365,0.743480832462554,0.804737854124365,
0.743480832462554,0.804737854124365,0.743480832462554,0.804737854124365,
0.743480832462554,0.804737854124365,0.743480832462554,0.804737854124365,
0.743480832462554,0.804737854124365,0.743480832462554,0.804737854124365,
0.743480832462554,0.804737854124365,0.743480832462554,0.804737854124365),
(1.,0.923879532511287,1.,0.923879532511287,1.,0.923879532511287,1.,0.923879532511287,
1.,0.923879532511287,1.,0.923879532511287,1.,0.923879532511287,1.,0.923879532511287,
1.,0.923879532511287,1.,0.923879532511287,1.,0.923879532511287,1.,0.923879532511287,
1.,0.923879532511287,1.,0.923879532511287,1.,0.923879532511287,1.,0.923879532511287,
1.,0.923879532511287,1.,0.923879532511287,1.,0.923879532511287,1.,0.923879532511287,
1.,0.923879532511287,1.,0.923879532511287,1.,0.923879532511287,1.,0.923879532511287,
1.,0.923879532511287,1.,0.923879532511287,1.,0.923879532511287,1.,0.923879532511287,
1.,0.923879532511287,1.,0.923879532511287,1.,0.923879532511287,1.,0.923879532511287,
1.)))
REPRESENTATION_ITEM('')
SURFACE()
);
#473=(
BOUNDED_SURFACE()
B_SPLINE_SURFACE(3,2,((#32391,#32392,#32393,#32394,#32395,#32396,#32397,
#32398,#32399,#32400,#32401,#32402,#32403,#32404,#32405,#32406,#32407,#32408,
#32409,#32410,#32411,#32412,#32413,#32414,#32415,#32416,#32417,#32418,#32419,
#32420,#32421,#32422,#32423,#32424,#32425,#32426,#32427,#32428,#32429,#32430,
#32431,#32432,#32433,#32434,#32435,#32436,#32437,#32438,#32439,#32440,#32441,
#32442,#32443,#32444,#32445,#32446,#32447,#32448,#32449,#32450,#32451,#32452,
#32453,#32454,#32455),(#32456,#32457,#32458,#32459,#32460,#32461,#32462,
#32463,#32464,#32465,#32466,#32467,#32468,#32469,#32470,#32471,#32472,#32473,
#32474,#32475,#32476,#32477,#32478,#32479,#32480,#32481,#32482,#32483,#32484,
#32485,#32486,#32487,#32488,#32489,#32490,#32491,#32492,#32493,#32494,#32495,
#32496,#32497,#32498,#32499,#32500,#32501,#32502,#32503,#32504,#32505,#32506,
#32507,#32508,#32509,#32510,#32511,#32512,#32513,#32514,#32515,#32516,#32517,
#32518,#32519,#32520),(#32521,#32522,#32523,#32524,#32525,#32526,#32527,
#32528,#32529,#32530,#32531,#32532,#32533,#32534,#32535,#32536,#32537,#32538,
#32539,#32540,#32541,#32542,#32543,#32544,#32545,#32546,#32547,#32548,#32549,
#32550,#32551,#32552,#32553,#32554,#32555,#32556,#32557,#32558,#32559,#32560,
#32561,#32562,#32563,#32564,#32565,#32566,#32567,#32568,#32569,#32570,#32571,
#32572,#32573,#32574,#32575,#32576,#32577,#32578,#32579,#32580,#32581,#32582,
#32583,#32584,#32585),(#32586,#32587,#32588,#32589,#32590,#32591,#32592,
#32593,#32594,#32595,#32596,#32597,#32598,#32599,#32600,#32601,#32602,#32603,
#32604,#32605,#32606,#32607,#32608,#32609,#32610,#32611,#32612,#32613,#32614,
#32615,#32616,#32617,#32618,#32619,#32620,#32621,#32622,#32623,#32624,#32625,
#32626,#32627,#32628,#32629,#32630,#32631,#32632,#32633,#32634,#32635,#32636,
#32637,#32638,#32639,#32640,#32641,#32642,#32643,#32644,#32645,#32646,#32647,
#32648,#32649,#32650)),.UNSPECIFIED.,.F.,.F.,.F.)
B_SPLINE_SURFACE_WITH_KNOTS((4,4),(3,2,2,2,2,2,2,2,2,2,2,2,2,2,2,2,2,2,
2,2,2,2,2,2,2,2,2,2,2,2,2,2,3),(0.,1.),(0.,0.03125,0.0625,0.09375,0.125,
0.15625,0.1875,0.21875,0.25,0.28125,0.3125,0.34375,0.375,0.40625,0.4375,
0.46875,0.5,0.53125,0.5625,0.59375,0.625,0.65625,0.6875,0.71875,0.75,0.78125,
0.8125,0.84375,0.875,0.90625,0.9375,0.96875,1.),.UNSPECIFIED.)
GEOMETRIC_REPRESENTATION_ITEM()
RATIONAL_B_SPLINE_SURFACE(((1.,0.923879532511287,1.,0.923879532511287,1.,
0.923879532511287,1.,0.923879532511287,1.,0.923879532511287,1.,0.923879532511287,
1.,0.923879532511287,1.,0.923879532511287,1.,0.923879532511287,1.,0.923879532511287,
1.,0.923879532511287,1.,0.923879532511287,1.,0.923879532511287,1.,0.923879532511287,
1.,0.923879532511287,1.,0.923879532511287,1.,0.923879532511287,1.,0.923879532511287,
1.,0.923879532511287,1.,0.923879532511287,1.,0.923879532511287,1.,0.923879532511287,
1.,0.923879532511287,1.,0.923879532511287,1.,0.923879532511287,1.,0.923879532511287,
1.,0.923879532511287,1.,0.923879532511287,1.,0.923879532511287,1.,0.923879532511287,
1.,0.923879532511287,1.,0.923879532511287,1.),(0.804737854124365,0.743480832462554,
0.804737854124365,0.743480832462554,0.804737854124365,0.743480832462554,
0.804737854124365,0.743480832462554,0.804737854124365,0.743480832462554,
0.804737854124365,0.743480832462554,0.804737854124365,0.743480832462554,
0.804737854124365,0.743480832462554,0.804737854124365,0.743480832462554,
0.804737854124365,0.743480832462554,0.804737854124365,0.743480832462554,
0.804737854124365,0.743480832462554,0.804737854124365,0.743480832462554,
0.804737854124365,0.743480832462554,0.804737854124365,0.743480832462554,
0.804737854124365,0.743480832462554,0.804737854124365,0.743480832462554,
0.804737854124365,0.743480832462554,0.804737854124365,0.743480832462554,
0.804737854124365,0.743480832462554,0.804737854124365,0.743480832462554,
0.804737854124365,0.743480832462554,0.804737854124365,0.743480832462554,
0.804737854124365,0.743480832462554,0.804737854124365,0.743480832462554,
0.804737854124365,0.743480832462554,0.804737854124365,0.743480832462554,
0.804737854124365,0.743480832462554,0.804737854124365,0.743480832462554,
0.804737854124365,0.743480832462554,0.804737854124365,0.743480832462554,
0.804737854124365,0.743480832462554,0.804737854124365),(0.804737854124365,
0.743480832462554,0.804737854124365,0.743480832462554,0.804737854124365,
0.743480832462554,0.804737854124365,0.743480832462554,0.804737854124365,
0.743480832462554,0.804737854124365,0.743480832462554,0.804737854124365,
0.743480832462554,0.804737854124365,0.743480832462554,0.804737854124365,
0.743480832462554,0.804737854124365,0.743480832462554,0.804737854124365,
0.743480832462554,0.804737854124365,0.743480832462554,0.804737854124365,
0.743480832462554,0.804737854124365,0.743480832462554,0.804737854124365,
0.743480832462554,0.804737854124365,0.743480832462554,0.804737854124365,
0.743480832462554,0.804737854124365,0.743480832462554,0.804737854124365,
0.743480832462554,0.804737854124365,0.743480832462554,0.804737854124365,
0.743480832462554,0.804737854124365,0.743480832462554,0.804737854124365,
0.743480832462554,0.804737854124365,0.743480832462554,0.804737854124365,
0.743480832462554,0.804737854124365,0.743480832462554,0.804737854124365,
0.743480832462554,0.804737854124365,0.743480832462554,0.804737854124365,
0.743480832462554,0.804737854124365,0.743480832462554,0.804737854124365,
0.743480832462554,0.804737854124365,0.743480832462554,0.804737854124365),
(1.,0.923879532511287,1.,0.923879532511287,1.,0.923879532511287,1.,0.923879532511287,
1.,0.923879532511287,1.,0.923879532511287,1.,0.923879532511287,1.,0.923879532511287,
1.,0.923879532511287,1.,0.923879532511287,1.,0.923879532511287,1.,0.923879532511287,
1.,0.923879532511287,1.,0.923879532511287,1.,0.923879532511287,1.,0.923879532511287,
1.,0.923879532511287,1.,0.923879532511287,1.,0.923879532511287,1.,0.923879532511287,
1.,0.923879532511287,1.,0.923879532511287,1.,0.923879532511287,1.,0.923879532511287,
1.,0.923879532511287,1.,0.923879532511287,1.,0.923879532511287,1.,0.923879532511287,
1.,0.923879532511287,1.,0.923879532511287,1.,0.923879532511287,1.,0.923879532511287,
1.)))
REPRESENTATION_ITEM('')
SURFACE()
);
#1002=PLANE('',#11111);
#1003=PLANE('',#11112);
#1522=FACE_OUTER_BOUND('',#2150,.T.);
#1523=FACE_OUTER_BOUND('',#2151,.T.);
#1524=FACE_OUTER_BOUND('',#2152,.T.);
#1525=FACE_OUTER_BOUND('',#2153,.T.);
#1526=FACE_OUTER_BOUND('',#2154,.T.);
#1527=FACE_OUTER_BOUND('',#2155,.T.);
#2150=EDGE_LOOP('',(#8980,#8981,#8982,#8983,#8984));
#2151=EDGE_LOOP('',(#8985,#8986,#8987,#8988,#8989));
#2152=EDGE_LOOP('',(#8990,#8991,#8992,#8993,#8994));
#2153=EDGE_LOOP('',(#8995,#8996,#8997,#8998,#8999));
#2154=EDGE_LOOP('',(#9000,#9001,#9002,#9003));
#2155=EDGE_LOOP('',(#9004,#9005,#9006,#9007));
#2544=CIRCLE('',#11103,0.6);
#2545=CIRCLE('',#11104,0.6);
#2546=CIRCLE('',#11105,0.6);
#2547=CIRCLE('',#11106,0.6);
#2548=CIRCLE('',#11107,0.6);
#2549=CIRCLE('',#11108,0.6);
#2550=CIRCLE('',#11109,0.6);
#2551=CIRCLE('',#11110,0.6);
#4946=VERTEX_POINT('',#31595);
#4947=VERTEX_POINT('',#31596);
#4948=VERTEX_POINT('',#31598);
#4949=VERTEX_POINT('',#31616);
#4950=VERTEX_POINT('',#31666);
#4951=VERTEX_POINT('',#31993);
#4952=VERTEX_POINT('',#32322);
#4953=VERTEX_POINT('',#32324);
#6303=EDGE_CURVE('',#4946,#4947,#2544,.T.);
#6304=EDGE_CURVE('',#4948,#4947,#203,.T.);
#6305=EDGE_CURVE('',#4949,#4948,#204,.T.);
#6306=EDGE_CURVE('',#4950,#4949,#2545,.T.);
#6307=EDGE_CURVE('',#4950,#4946,#205,.T.);
#6308=EDGE_CURVE('',#4951,#4950,#2546,.T.);
#6309=EDGE_CURVE('',#4951,#4949,#206,.T.);
#6310=EDGE_CURVE('',#4949,#4948,#207,.T.);
#6311=EDGE_CURVE('',#4948,#4946,#2547,.T.);
#6312=EDGE_CURVE('',#4952,#4951,#2548,.T.);
#6313=EDGE_CURVE('',#4952,#4953,#208,.T.);
#6314=EDGE_CURVE('',#4953,#4948,#2549,.T.);
#6315=EDGE_CURVE('',#4949,#4952,#2550,.T.);
#6316=EDGE_CURVE('',#4947,#4953,#2551,.T.);
#8980=ORIENTED_EDGE('',*,*,#6303,.T.);
#8981=ORIENTED_EDGE('',*,*,#6304,.F.);
#8982=ORIENTED_EDGE('',*,*,#6305,.F.);
#8983=ORIENTED_EDGE('',*,*,#6306,.F.);
#8984=ORIENTED_EDGE('',*,*,#6307,.T.);
#8985=ORIENTED_EDGE('',*,*,#6307,.F.);
#8986=ORIENTED_EDGE('',*,*,#6308,.F.);
#8987=ORIENTED_EDGE('',*,*,#6309,.T.);
#8988=ORIENTED_EDGE('',*,*,#6310,.T.);
#8989=ORIENTED_EDGE('',*,*,#6311,.T.);
#8990=ORIENTED_EDGE('',*,*,#6309,.F.);
#8991=ORIENTED_EDGE('',*,*,#6312,.F.);
#8992=ORIENTED_EDGE('',*,*,#6313,.T.);
#8993=ORIENTED_EDGE('',*,*,#6314,.T.);
#8994=ORIENTED_EDGE('',*,*,#6310,.F.);
#8995=ORIENTED_EDGE('',*,*,#6313,.F.);
#8996=ORIENTED_EDGE('',*,*,#6315,.F.);
#8997=ORIENTED_EDGE('',*,*,#6305,.T.);
#8998=ORIENTED_EDGE('',*,*,#6304,.T.);
#8999=ORIENTED_EDGE('',*,*,#6316,.T.);
#9000=ORIENTED_EDGE('',*,*,#6316,.F.);
#9001=ORIENTED_EDGE('',*,*,#6303,.F.);
#9002=ORIENTED_EDGE('',*,*,#6311,.F.);
#9003=ORIENTED_EDGE('',*,*,#6314,.F.);
#9004=ORIENTED_EDGE('',*,*,#6315,.T.);
#9005=ORIENTED_EDGE('',*,*,#6312,.T.);
#9006=ORIENTED_EDGE('',*,*,#6308,.T.);
#9007=ORIENTED_EDGE('',*,*,#6306,.T.);
#9888=ADVANCED_FACE('',(#1522),#470,.F.);
#9889=ADVANCED_FACE('',(#1523),#471,.F.);
#9890=ADVANCED_FACE('',(#1524),#472,.F.);
#9891=ADVANCED_FACE('',(#1525),#473,.F.);
#9892=ADVANCED_FACE('',(#1526),#1002,.F.);
#9893=ADVANCED_FACE('',(#1527),#1003,.T.);
#9963=CLOSED_SHELL('',(#9888,#9889,#9890,#9891,#9892,#9893));
#11102=AXIS2_PLACEMENT_3D('',#31334,#13618,#13619);
#11103=AXIS2_PLACEMENT_3D('',#31597,#13620,#13621);
#11104=AXIS2_PLACEMENT_3D('',#31667,#13622,#13623);
#11105=AXIS2_PLACEMENT_3D('',#31994,#13624,#13625);
#11106=AXIS2_PLACEMENT_3D('',#32061,#13626,#13627);
#11107=AXIS2_PLACEMENT_3D('',#32323,#13628,#13629);
#11108=AXIS2_PLACEMENT_3D('',#32390,#13630,#13631);
#11109=AXIS2_PLACEMENT_3D('',#32651,#13632,#13633);
#11110=AXIS2_PLACEMENT_3D('',#32652,#13634,#13635);
#11111=AXIS2_PLACEMENT_3D('',#32653,#13636,#13637);
#11112=AXIS2_PLACEMENT_3D('',#32654,#13638,#13639);
#13618=DIRECTION('axis',(0.,0.,1.));
#13619=DIRECTION('refdir',(1.,0.,0.));
#13620=DIRECTION('center_axis',(1.,0.,5.58637014214901E-14));
#13621=DIRECTION('ref_axis',(5.58637014214901E-14,0.,-1.));
#13622=DIRECTION('center_axis',(1.,0.,0.));
#13623=DIRECTION('ref_axis',(0.,0.,-1.));
#13624=DIRECTION('center_axis',(1.,0.,0.));
#13625=DIRECTION('ref_axis',(0.,0.,-1.));
#13626=DIRECTION('center_axis',(1.,0.,5.58637014214901E-14));
#13627=DIRECTION('ref_axis',(5.58637014214901E-14,0.,-1.));
#13628=DIRECTION('center_axis',(1.,0.,0.));
#13629=DIRECTION('ref_axis',(0.,0.,-1.));
#13630=DIRECTION('center_axis',(1.,0.,5.58637014214901E-14));
#13631=DIRECTION('ref_axis',(5.58637014214901E-14,0.,-1.));
#13632=DIRECTION('center_axis',(1.,0.,0.));
#13633=DIRECTION('ref_axis',(0.,0.,-1.));
#13634=DIRECTION('center_axis',(1.,0.,5.58637014214901E-14));
#13635=DIRECTION('ref_axis',(5.58637014214901E-14,0.,-1.));
#13636=DIRECTION('center_axis',(1.,0.,5.58637014214901E-14));
#13637=DIRECTION('ref_axis',(5.58637014214901E-14,0.,-1.));
#13638=DIRECTION('center_axis',(1.,0.,0.));
#13639=DIRECTION('ref_axis',(0.,0.,-1.));
#31334=CARTESIAN_POINT('',(0.,0.,0.));
#31335=CARTESIAN_POINT('Ctrl Pts',(0.,0.,13.55));
#31336=CARTESIAN_POINT('Ctrl Pts',(-5.61259377015544,0.0749999999999998,
13.55));
#31337=CARTESIAN_POINT('Ctrl Pts',(-9.58129688507772,0.15,9.58129688507772));
#31338=CARTESIAN_POINT('Ctrl Pts',(-13.55,0.225,5.61259377015544));
#31339=CARTESIAN_POINT('Ctrl Pts',(-13.55,0.299999999999999,8.29698206422332E-16));
#31340=CARTESIAN_POINT('Ctrl Pts',(-13.55,0.374999999999999,-5.61259377015544));
#31341=CARTESIAN_POINT('Ctrl Pts',(-9.58129688507772,0.449999999999999,
-9.58129688507772));
#31342=CARTESIAN_POINT('Ctrl Pts',(-5.61259377015544,0.524999999999999,
-13.55));
#31343=CARTESIAN_POINT('Ctrl Pts',(-1.65939641284466E-15,0.599999999999999,
-13.55));
#31344=CARTESIAN_POINT('Ctrl Pts',(5.61259377015543,0.674999999999998,-13.55));
#31345=CARTESIAN_POINT('Ctrl Pts',(9.58129688507772,0.749999999999998,-9.58129688507772));
#31346=CARTESIAN_POINT('Ctrl Pts',(13.55,0.824999999999998,-5.61259377015545));
#31347=CARTESIAN_POINT('Ctrl Pts',(13.55,0.899999999999998,-2.489094619267E-15));
#31348=CARTESIAN_POINT('Ctrl Pts',(13.55,0.974999999999998,5.61259377015544));
#31349=CARTESIAN_POINT('Ctrl Pts',(9.58129688507772,1.05,9.58129688507772));
#31350=CARTESIAN_POINT('Ctrl Pts',(5.61259377015545,1.125,13.55));
#31351=CARTESIAN_POINT('Ctrl Pts',(0.,1.2,13.55));
#31352=CARTESIAN_POINT('Ctrl Pts',(-5.61259377015544,1.275,13.55));
#31353=CARTESIAN_POINT('Ctrl Pts',(-9.58129688507772,1.35,9.58129688507772));
#31354=CARTESIAN_POINT('Ctrl Pts',(-13.55,1.425,5.61259377015544));
#31355=CARTESIAN_POINT('Ctrl Pts',(-13.55,1.5,8.29698206422332E-16));
#31356=CARTESIAN_POINT('Ctrl Pts',(-13.55,1.575,-5.61259377015544));
#31357=CARTESIAN_POINT('Ctrl Pts',(-9.58129688507772,1.65,-9.58129688507772));
#31358=CARTESIAN_POINT('Ctrl Pts',(-5.61259377015544,1.725,-13.55));
#31359=CARTESIAN_POINT('Ctrl Pts',(-1.65939641284466E-15,1.8,-13.55));
#31360=CARTESIAN_POINT('Ctrl Pts',(5.61259377015543,1.875,-13.55));
#31361=CARTESIAN_POINT('Ctrl Pts',(9.58129688507772,1.95,-9.58129688507772));
#31362=CARTESIAN_POINT('Ctrl Pts',(13.55,2.025,-5.61259377015545));
#31363=CARTESIAN_POINT('Ctrl Pts',(13.55,2.1,-2.489094619267E-15));
#31364=CARTESIAN_POINT('Ctrl Pts',(13.55,2.17499999999999,5.61259377015544));
#31365=CARTESIAN_POINT('Ctrl Pts',(9.58129688507772,2.25,9.58129688507772));
#31366=CARTESIAN_POINT('Ctrl Pts',(5.61259377015545,2.32499999999999,13.55));
#31367=CARTESIAN_POINT('Ctrl Pts',(0.,2.39999999999999,13.55));
#31368=CARTESIAN_POINT('Ctrl Pts',(-5.61259377015544,2.47499999999999,13.55));
#31369=CARTESIAN_POINT('Ctrl Pts',(-9.58129688507772,2.54999999999999,9.58129688507772));
#31370=CARTESIAN_POINT('Ctrl Pts',(-13.55,2.62499999999999,5.61259377015544));
#31371=CARTESIAN_POINT('Ctrl Pts',(-13.55,2.69999999999999,8.29698206422332E-16));
#31372=CARTESIAN_POINT('Ctrl Pts',(-13.55,2.77499999999999,-5.61259377015544));
#31373=CARTESIAN_POINT('Ctrl Pts',(-9.58129688507772,2.84999999999999,-9.58129688507772));
#31374=CARTESIAN_POINT('Ctrl Pts',(-5.61259377015544,2.92499999999999,-13.55));
#31375=CARTESIAN_POINT('Ctrl Pts',(-1.65939641284466E-15,2.99999999999999,
-13.55));
#31376=CARTESIAN_POINT('Ctrl Pts',(5.61259377015543,3.07499999999999,-13.55));
#31377=CARTESIAN_POINT('Ctrl Pts',(9.58129688507772,3.14999999999999,-9.58129688507772));
#31378=CARTESIAN_POINT('Ctrl Pts',(13.55,3.22499999999999,-5.61259377015545));
#31379=CARTESIAN_POINT('Ctrl Pts',(13.55,3.29999999999999,-2.489094619267E-15));
#31380=CARTESIAN_POINT('Ctrl Pts',(13.55,3.37499999999999,5.61259377015544));
#31381=CARTESIAN_POINT('Ctrl Pts',(9.58129688507772,3.44999999999999,9.58129688507772));
#31382=CARTESIAN_POINT('Ctrl Pts',(5.61259377015545,3.52499999999999,13.55));
#31383=CARTESIAN_POINT('Ctrl Pts',(0.,3.59999999999999,13.55));
#31384=CARTESIAN_POINT('Ctrl Pts',(-5.61259377015544,3.67499999999999,13.55));
#31385=CARTESIAN_POINT('Ctrl Pts',(-9.58129688507772,3.74999999999999,9.58129688507772));
#31386=CARTESIAN_POINT('Ctrl Pts',(-13.55,3.82499999999999,5.61259377015544));
#31387=CARTESIAN_POINT('Ctrl Pts',(-13.55,3.89999999999999,8.29698206422332E-16));
#31388=CARTESIAN_POINT('Ctrl Pts',(-13.55,3.97499999999999,-5.61259377015544));
#31389=CARTESIAN_POINT('Ctrl Pts',(-9.58129688507772,4.04999999999999,-9.58129688507772));
#31390=CARTESIAN_POINT('Ctrl Pts',(-5.61259377015544,4.12499999999999,-13.55));
#31391=CARTESIAN_POINT('Ctrl Pts',(-1.65939641284466E-15,4.19999999999999,
-13.55));
#31392=CARTESIAN_POINT('Ctrl Pts',(5.61259377015543,4.27499999999999,-13.55));
#31393=CARTESIAN_POINT('Ctrl Pts',(9.58129688507772,4.34999999999999,-9.58129688507772));
#31394=CARTESIAN_POINT('Ctrl Pts',(13.55,4.42499999999999,-5.61259377015545));
#31395=CARTESIAN_POINT('Ctrl Pts',(13.55,4.49999999999999,-2.489094619267E-15));
#31396=CARTESIAN_POINT('Ctrl Pts',(13.55,4.57499999999999,5.61259377015544));
#31397=CARTESIAN_POINT('Ctrl Pts',(9.58129688507772,4.64999999999999,9.58129688507772));
#31398=CARTESIAN_POINT('Ctrl Pts',(5.61259377015545,4.72499999999999,13.55));
#31399=CARTESIAN_POINT('Ctrl Pts',(0.,4.79999999999999,13.55));
#31400=CARTESIAN_POINT('Ctrl Pts',(0.,0.351471862576143,13.55));
#31401=CARTESIAN_POINT('Ctrl Pts',(-5.61259377015544,0.426471862576143,
13.55));
#31402=CARTESIAN_POINT('Ctrl Pts',(-9.58129688507772,0.501471862576143,
9.58129688507772));
#31403=CARTESIAN_POINT('Ctrl Pts',(-13.55,0.576471862576143,5.61259377015544));
#31404=CARTESIAN_POINT('Ctrl Pts',(-13.55,0.651471862576142,8.29698206422332E-16));
#31405=CARTESIAN_POINT('Ctrl Pts',(-13.55,0.726471862576142,-5.61259377015544));
#31406=CARTESIAN_POINT('Ctrl Pts',(-9.58129688507772,0.801471862576142,
-9.58129688507772));
#31407=CARTESIAN_POINT('Ctrl Pts',(-5.61259377015544,0.876471862576142,
-13.55));
#31408=CARTESIAN_POINT('Ctrl Pts',(-1.65939641284466E-15,0.951471862576142,
-13.55));
#31409=CARTESIAN_POINT('Ctrl Pts',(5.61259377015544,1.02647186257614,-13.55));
#31410=CARTESIAN_POINT('Ctrl Pts',(9.58129688507772,1.10147186257614,-9.58129688507772));
#31411=CARTESIAN_POINT('Ctrl Pts',(13.55,1.17647186257614,-5.61259377015545));
#31412=CARTESIAN_POINT('Ctrl Pts',(13.55,1.25147186257614,-2.489094619267E-15));
#31413=CARTESIAN_POINT('Ctrl Pts',(13.55,1.32647186257614,5.61259377015544));
#31414=CARTESIAN_POINT('Ctrl Pts',(9.58129688507772,1.40147186257614,9.58129688507772));
#31415=CARTESIAN_POINT('Ctrl Pts',(5.61259377015545,1.47647186257614,13.55));
#31416=CARTESIAN_POINT('Ctrl Pts',(0.,1.55147186257614,13.55));
#31417=CARTESIAN_POINT('Ctrl Pts',(-5.61259377015544,1.62647186257614,13.55));
#31418=CARTESIAN_POINT('Ctrl Pts',(-9.58129688507772,1.70147186257614,9.58129688507772));
#31419=CARTESIAN_POINT('Ctrl Pts',(-13.55,1.77647186257614,5.61259377015544));
#31420=CARTESIAN_POINT('Ctrl Pts',(-13.55,1.85147186257614,8.29698206422332E-16));
#31421=CARTESIAN_POINT('Ctrl Pts',(-13.55,1.92647186257614,-5.61259377015544));
#31422=CARTESIAN_POINT('Ctrl Pts',(-9.58129688507772,2.00147186257614,-9.58129688507772));
#31423=CARTESIAN_POINT('Ctrl Pts',(-5.61259377015544,2.07647186257614,-13.55));
#31424=CARTESIAN_POINT('Ctrl Pts',(-1.65939641284466E-15,2.15147186257614,
-13.55));
#31425=CARTESIAN_POINT('Ctrl Pts',(5.61259377015544,2.22647186257614,-13.55));
#31426=CARTESIAN_POINT('Ctrl Pts',(9.58129688507772,2.30147186257614,-9.58129688507772));
#31427=CARTESIAN_POINT('Ctrl Pts',(13.55,2.37647186257614,-5.61259377015545));
#31428=CARTESIAN_POINT('Ctrl Pts',(13.55,2.45147186257614,-2.489094619267E-15));
#31429=CARTESIAN_POINT('Ctrl Pts',(13.55,2.52647186257614,5.61259377015544));
#31430=CARTESIAN_POINT('Ctrl Pts',(9.58129688507772,2.60147186257614,9.58129688507772));
#31431=CARTESIAN_POINT('Ctrl Pts',(5.61259377015545,2.67647186257614,13.55));
#31432=CARTESIAN_POINT('Ctrl Pts',(0.,2.75147186257614,13.55));
#31433=CARTESIAN_POINT('Ctrl Pts',(-5.61259377015544,2.82647186257614,13.55));
#31434=CARTESIAN_POINT('Ctrl Pts',(-9.58129688507772,2.90147186257614,9.58129688507772));
#31435=CARTESIAN_POINT('Ctrl Pts',(-13.55,2.97647186257614,5.61259377015544));
#31436=CARTESIAN_POINT('Ctrl Pts',(-13.55,3.05147186257614,8.29698206422332E-16));
#31437=CARTESIAN_POINT('Ctrl Pts',(-13.55,3.12647186257614,-5.61259377015544));
#31438=CARTESIAN_POINT('Ctrl Pts',(-9.58129688507772,3.20147186257614,-9.58129688507772));
#31439=CARTESIAN_POINT('Ctrl Pts',(-5.61259377015544,3.27647186257614,-13.55));
#31440=CARTESIAN_POINT('Ctrl Pts',(-1.65939641284466E-15,3.35147186257614,
-13.55));
#31441=CARTESIAN_POINT('Ctrl Pts',(5.61259377015544,3.42647186257614,-13.55));
#31442=CARTESIAN_POINT('Ctrl Pts',(9.58129688507772,3.50147186257614,-9.58129688507772));
#31443=CARTESIAN_POINT('Ctrl Pts',(13.55,3.57647186257614,-5.61259377015545));
#31444=CARTESIAN_POINT('Ctrl Pts',(13.55,3.65147186257614,-2.489094619267E-15));
#31445=CARTESIAN_POINT('Ctrl Pts',(13.55,3.72647186257614,5.61259377015544));
#31446=CARTESIAN_POINT('Ctrl Pts',(9.58129688507772,3.80147186257614,9.58129688507772));
#31447=CARTESIAN_POINT('Ctrl Pts',(5.61259377015545,3.87647186257614,13.55));
#31448=CARTESIAN_POINT('Ctrl Pts',(0.,3.95147186257614,13.55));
#31449=CARTESIAN_POINT('Ctrl Pts',(-5.61259377015544,4.02647186257614,13.55));
#31450=CARTESIAN_POINT('Ctrl Pts',(-9.58129688507772,4.10147186257613,9.58129688507772));
#31451=CARTESIAN_POINT('Ctrl Pts',(-13.55,4.17647186257613,5.61259377015544));
#31452=CARTESIAN_POINT('Ctrl Pts',(-13.55,4.25147186257614,8.29698206422332E-16));
#31453=CARTESIAN_POINT('Ctrl Pts',(-13.55,4.32647186257613,-5.61259377015544));
#31454=CARTESIAN_POINT('Ctrl Pts',(-9.58129688507772,4.40147186257613,-9.58129688507772));
#31455=CARTESIAN_POINT('Ctrl Pts',(-5.61259377015544,4.47647186257614,-13.55));
#31456=CARTESIAN_POINT('Ctrl Pts',(-1.65939641284466E-15,4.55147186257613,
-13.55));
#31457=CARTESIAN_POINT('Ctrl Pts',(5.61259377015544,4.62647186257613,-13.55));
#31458=CARTESIAN_POINT('Ctrl Pts',(9.58129688507772,4.70147186257613,-9.58129688507772));
#31459=CARTESIAN_POINT('Ctrl Pts',(13.55,4.77647186257613,-5.61259377015545));
#31460=CARTESIAN_POINT('Ctrl Pts',(13.55,4.85147186257613,-2.489094619267E-15));
#31461=CARTESIAN_POINT('Ctrl Pts',(13.55,4.92647186257613,5.61259377015544));
#31462=CARTESIAN_POINT('Ctrl Pts',(9.58129688507772,5.00147186257613,9.58129688507772));
#31463=CARTESIAN_POINT('Ctrl Pts',(5.61259377015545,5.07647186257613,13.55));
#31464=CARTESIAN_POINT('Ctrl Pts',(0.,5.15147186257613,13.55));
#31465=CARTESIAN_POINT('Ctrl Pts',(0.,0.6,13.7985281374239));
#31466=CARTESIAN_POINT('Ctrl Pts',(-5.71553749530772,0.675,13.7985281374239));
#31467=CARTESIAN_POINT('Ctrl Pts',(-9.75703281636579,0.75,9.75703281636579));
#31468=CARTESIAN_POINT('Ctrl Pts',(-13.7985281374239,0.825,5.71553749530772));
#31469=CARTESIAN_POINT('Ctrl Pts',(-13.7985281374239,0.9,8.44916165822041E-16));
#31470=CARTESIAN_POINT('Ctrl Pts',(-13.7985281374239,0.974999999999999,
-5.71553749530772));
#31471=CARTESIAN_POINT('Ctrl Pts',(-9.75703281636579,1.05,-9.75703281636579));
#31472=CARTESIAN_POINT('Ctrl Pts',(-5.71553749530773,1.125,-13.7985281374239));
#31473=CARTESIAN_POINT('Ctrl Pts',(-1.68983233164408E-15,1.2,-13.7985281374239));
#31474=CARTESIAN_POINT('Ctrl Pts',(5.71553749530772,1.275,-13.7985281374239));
#31475=CARTESIAN_POINT('Ctrl Pts',(9.75703281636579,1.35,-9.75703281636579));
#31476=CARTESIAN_POINT('Ctrl Pts',(13.7985281374239,1.425,-5.71553749530773));
#31477=CARTESIAN_POINT('Ctrl Pts',(13.7985281374239,1.5,-2.53474849746612E-15));
#31478=CARTESIAN_POINT('Ctrl Pts',(13.7985281374239,1.575,5.71553749530773));
#31479=CARTESIAN_POINT('Ctrl Pts',(9.75703281636579,1.65,9.75703281636579));
#31480=CARTESIAN_POINT('Ctrl Pts',(5.71553749530774,1.725,13.7985281374239));
#31481=CARTESIAN_POINT('Ctrl Pts',(0.,1.8,13.7985281374239));
#31482=CARTESIAN_POINT('Ctrl Pts',(-5.71553749530772,1.875,13.7985281374239));
#31483=CARTESIAN_POINT('Ctrl Pts',(-9.75703281636579,1.95,9.75703281636579));
#31484=CARTESIAN_POINT('Ctrl Pts',(-13.7985281374239,2.025,5.71553749530772));
#31485=CARTESIAN_POINT('Ctrl Pts',(-13.7985281374239,2.1,8.44916165822041E-16));
#31486=CARTESIAN_POINT('Ctrl Pts',(-13.7985281374239,2.175,-5.71553749530772));
#31487=CARTESIAN_POINT('Ctrl Pts',(-9.75703281636579,2.25,-9.75703281636579));
#31488=CARTESIAN_POINT('Ctrl Pts',(-5.71553749530773,2.325,-13.7985281374239));
#31489=CARTESIAN_POINT('Ctrl Pts',(-1.68983233164408E-15,2.4,-13.7985281374239));
#31490=CARTESIAN_POINT('Ctrl Pts',(5.71553749530772,2.475,-13.7985281374239));
#31491=CARTESIAN_POINT('Ctrl Pts',(9.75703281636579,2.55,-9.75703281636579));
#31492=CARTESIAN_POINT('Ctrl Pts',(13.7985281374239,2.625,-5.71553749530773));
#31493=CARTESIAN_POINT('Ctrl Pts',(13.7985281374239,2.7,-2.53474849746612E-15));
#31494=CARTESIAN_POINT('Ctrl Pts',(13.7985281374239,2.775,5.71553749530773));
#31495=CARTESIAN_POINT('Ctrl Pts',(9.75703281636579,2.85,9.75703281636579));
#31496=CARTESIAN_POINT('Ctrl Pts',(5.71553749530774,2.92499999999999,13.7985281374239));
#31497=CARTESIAN_POINT('Ctrl Pts',(0.,2.99999999999999,13.7985281374239));
#31498=CARTESIAN_POINT('Ctrl Pts',(-5.71553749530772,3.075,13.7985281374239));
#31499=CARTESIAN_POINT('Ctrl Pts',(-9.75703281636579,3.14999999999999,9.75703281636579));
#31500=CARTESIAN_POINT('Ctrl Pts',(-13.7985281374239,3.22499999999999,5.71553749530772));
#31501=CARTESIAN_POINT('Ctrl Pts',(-13.7985281374239,3.29999999999999,8.44916165822041E-16));
#31502=CARTESIAN_POINT('Ctrl Pts',(-13.7985281374239,3.37499999999999,-5.71553749530772));
#31503=CARTESIAN_POINT('Ctrl Pts',(-9.75703281636579,3.44999999999999,-9.75703281636579));
#31504=CARTESIAN_POINT('Ctrl Pts',(-5.71553749530773,3.52499999999999,-13.7985281374239));
#31505=CARTESIAN_POINT('Ctrl Pts',(-1.68983233164408E-15,3.59999999999999,
-13.7985281374239));
#31506=CARTESIAN_POINT('Ctrl Pts',(5.71553749530772,3.67499999999999,-13.7985281374239));
#31507=CARTESIAN_POINT('Ctrl Pts',(9.75703281636579,3.74999999999999,-9.75703281636579));
#31508=CARTESIAN_POINT('Ctrl Pts',(13.7985281374239,3.82499999999999,-5.71553749530773));
#31509=CARTESIAN_POINT('Ctrl Pts',(13.7985281374239,3.89999999999999,-2.53474849746612E-15));
#31510=CARTESIAN_POINT('Ctrl Pts',(13.7985281374239,3.97499999999999,5.71553749530773));
#31511=CARTESIAN_POINT('Ctrl Pts',(9.75703281636579,4.04999999999999,9.75703281636579));
#31512=CARTESIAN_POINT('Ctrl Pts',(5.71553749530774,4.12499999999999,13.7985281374239));
#31513=CARTESIAN_POINT('Ctrl Pts',(0.,4.19999999999999,13.7985281374239));
#31514=CARTESIAN_POINT('Ctrl Pts',(-5.71553749530772,4.27499999999999,13.7985281374239));
#31515=CARTESIAN_POINT('Ctrl Pts',(-9.75703281636579,4.34999999999999,9.75703281636579));
#31516=CARTESIAN_POINT('Ctrl Pts',(-13.7985281374239,4.42499999999999,5.71553749530772));
#31517=CARTESIAN_POINT('Ctrl Pts',(-13.7985281374239,4.49999999999999,8.44916165822041E-16));
#31518=CARTESIAN_POINT('Ctrl Pts',(-13.7985281374239,4.57499999999999,-5.71553749530772));
#31519=CARTESIAN_POINT('Ctrl Pts',(-9.75703281636579,4.64999999999999,-9.75703281636579));
#31520=CARTESIAN_POINT('Ctrl Pts',(-5.71553749530773,4.72499999999999,-13.7985281374239));
#31521=CARTESIAN_POINT('Ctrl Pts',(-1.68983233164408E-15,4.79999999999999,
-13.7985281374239));
#31522=CARTESIAN_POINT('Ctrl Pts',(5.71553749530772,4.87499999999999,-13.7985281374239));
#31523=CARTESIAN_POINT('Ctrl Pts',(9.75703281636579,4.94999999999999,-9.75703281636579));
#31524=CARTESIAN_POINT('Ctrl Pts',(13.7985281374239,5.02499999999999,-5.71553749530773));
#31525=CARTESIAN_POINT('Ctrl Pts',(13.7985281374239,5.09999999999999,-2.53474849746612E-15));
#31526=CARTESIAN_POINT('Ctrl Pts',(13.7985281374239,5.17499999999999,5.71553749530773));
#31527=CARTESIAN_POINT('Ctrl Pts',(9.75703281636579,5.24999999999999,9.75703281636579));
#31528=CARTESIAN_POINT('Ctrl Pts',(5.71553749530774,5.32499999999999,13.7985281374239));
#31529=CARTESIAN_POINT('Ctrl Pts',(0.,5.39999999999999,13.7985281374239));
#31530=CARTESIAN_POINT('Ctrl Pts',(0.,0.6,14.15));
#31531=CARTESIAN_POINT('Ctrl Pts',(-5.8611219075793,0.675,14.15));
#31532=CARTESIAN_POINT('Ctrl Pts',(-10.0055609537896,0.75,10.0055609537896));
#31533=CARTESIAN_POINT('Ctrl Pts',(-14.15,0.825,5.8611219075793));
#31534=CARTESIAN_POINT('Ctrl Pts',(-14.15,0.9,8.66437610396752E-16));
#31535=CARTESIAN_POINT('Ctrl Pts',(-14.15,0.974999999999999,-5.86112190757929));
#31536=CARTESIAN_POINT('Ctrl Pts',(-10.0055609537896,1.05,-10.0055609537896));
#31537=CARTESIAN_POINT('Ctrl Pts',(-5.8611219075793,1.125,-14.15));
#31538=CARTESIAN_POINT('Ctrl Pts',(-1.7328752207935E-15,1.2,-14.15));
#31539=CARTESIAN_POINT('Ctrl Pts',(5.86112190757929,1.275,-14.15));
#31540=CARTESIAN_POINT('Ctrl Pts',(10.0055609537896,1.35,-10.0055609537896));
#31541=CARTESIAN_POINT('Ctrl Pts',(14.15,1.425,-5.8611219075793));
#31542=CARTESIAN_POINT('Ctrl Pts',(14.15,1.5,-2.59931283119026E-15));
#31543=CARTESIAN_POINT('Ctrl Pts',(14.15,1.575,5.8611219075793));
#31544=CARTESIAN_POINT('Ctrl Pts',(10.0055609537896,1.65,10.0055609537896));
#31545=CARTESIAN_POINT('Ctrl Pts',(5.8611219075793,1.725,14.15));
#31546=CARTESIAN_POINT('Ctrl Pts',(0.,1.8,14.15));
#31547=CARTESIAN_POINT('Ctrl Pts',(-5.8611219075793,1.875,14.15));
#31548=CARTESIAN_POINT('Ctrl Pts',(-10.0055609537896,1.95,10.0055609537896));
#31549=CARTESIAN_POINT('Ctrl Pts',(-14.15,2.025,5.8611219075793));
#31550=CARTESIAN_POINT('Ctrl Pts',(-14.15,2.1,8.66437610396752E-16));
#31551=CARTESIAN_POINT('Ctrl Pts',(-14.15,2.175,-5.86112190757929));
#31552=CARTESIAN_POINT('Ctrl Pts',(-10.0055609537896,2.25,-10.0055609537896));
#31553=CARTESIAN_POINT('Ctrl Pts',(-5.8611219075793,2.325,-14.15));
#31554=CARTESIAN_POINT('Ctrl Pts',(-1.7328752207935E-15,2.4,-14.15));
#31555=CARTESIAN_POINT('Ctrl Pts',(5.86112190757929,2.475,-14.15));
#31556=CARTESIAN_POINT('Ctrl Pts',(10.0055609537896,2.55,-10.0055609537896));
#31557=CARTESIAN_POINT('Ctrl Pts',(14.15,2.625,-5.8611219075793));
#31558=CARTESIAN_POINT('Ctrl Pts',(14.15,2.7,-2.59931283119026E-15));
#31559=CARTESIAN_POINT('Ctrl Pts',(14.15,2.775,5.8611219075793));
#31560=CARTESIAN_POINT('Ctrl Pts',(10.0055609537896,2.85,10.0055609537896));
#31561=CARTESIAN_POINT('Ctrl Pts',(5.8611219075793,2.92499999999999,14.15));
#31562=CARTESIAN_POINT('Ctrl Pts',(0.,2.99999999999999,14.15));
#31563=CARTESIAN_POINT('Ctrl Pts',(-5.8611219075793,3.07499999999999,14.15));
#31564=CARTESIAN_POINT('Ctrl Pts',(-10.0055609537896,3.15,10.0055609537896));
#31565=CARTESIAN_POINT('Ctrl Pts',(-14.15,3.22499999999999,5.8611219075793));
#31566=CARTESIAN_POINT('Ctrl Pts',(-14.15,3.29999999999999,8.66437610396752E-16));
#31567=CARTESIAN_POINT('Ctrl Pts',(-14.15,3.37499999999999,-5.86112190757929));
#31568=CARTESIAN_POINT('Ctrl Pts',(-10.0055609537896,3.44999999999999,-10.0055609537896));
#31569=CARTESIAN_POINT('Ctrl Pts',(-5.8611219075793,3.52499999999999,-14.15));
#31570=CARTESIAN_POINT('Ctrl Pts',(-1.7328752207935E-15,3.59999999999999,
-14.15));
#31571=CARTESIAN_POINT('Ctrl Pts',(5.86112190757929,3.67499999999999,-14.15));
#31572=CARTESIAN_POINT('Ctrl Pts',(10.0055609537896,3.74999999999999,-10.0055609537896));
#31573=CARTESIAN_POINT('Ctrl Pts',(14.15,3.82499999999999,-5.8611219075793));
#31574=CARTESIAN_POINT('Ctrl Pts',(14.15,3.89999999999999,-2.59931283119026E-15));
#31575=CARTESIAN_POINT('Ctrl Pts',(14.15,3.97499999999999,5.8611219075793));
#31576=CARTESIAN_POINT('Ctrl Pts',(10.0055609537896,4.04999999999999,10.0055609537896));
#31577=CARTESIAN_POINT('Ctrl Pts',(5.8611219075793,4.12499999999999,14.15));
#31578=CARTESIAN_POINT('Ctrl Pts',(0.,4.19999999999999,14.15));
#31579=CARTESIAN_POINT('Ctrl Pts',(-5.8611219075793,4.27499999999999,14.15));
#31580=CARTESIAN_POINT('Ctrl Pts',(-10.0055609537896,4.34999999999999,10.0055609537896));
#31581=CARTESIAN_POINT('Ctrl Pts',(-14.15,4.42499999999999,5.8611219075793));
#31582=CARTESIAN_POINT('Ctrl Pts',(-14.15,4.49999999999999,8.66437610396752E-16));
#31583=CARTESIAN_POINT('Ctrl Pts',(-14.15,4.57499999999999,-5.86112190757929));
#31584=CARTESIAN_POINT('Ctrl Pts',(-10.0055609537896,4.64999999999999,-10.0055609537896));
#31585=CARTESIAN_POINT('Ctrl Pts',(-5.8611219075793,4.72499999999999,-14.15));
#31586=CARTESIAN_POINT('Ctrl Pts',(-1.7328752207935E-15,4.79999999999999,
-14.15));
#31587=CARTESIAN_POINT('Ctrl Pts',(5.86112190757929,4.87499999999999,-14.15));
#31588=CARTESIAN_POINT('Ctrl Pts',(10.0055609537896,4.94999999999999,-10.0055609537896));
#31589=CARTESIAN_POINT('Ctrl Pts',(14.15,5.02499999999999,-5.8611219075793));
#31590=CARTESIAN_POINT('Ctrl Pts',(14.15,5.09999999999999,-2.59931283119026E-15));
#31591=CARTESIAN_POINT('Ctrl Pts',(14.15,5.17499999999999,5.8611219075793));
#31592=CARTESIAN_POINT('Ctrl Pts',(10.0055609537896,5.24999999999999,10.0055609537896));
#31593=CARTESIAN_POINT('Ctrl Pts',(5.8611219075793,5.32499999999999,14.15));
#31594=CARTESIAN_POINT('Ctrl Pts',(0.,5.39999999999999,14.15));
#31595=CARTESIAN_POINT('',(-3.71838991479217E-13,4.79999999999999,13.55));
#31596=CARTESIAN_POINT('',(-3.86571311453075E-13,5.39999999999999,14.15));
#31597=CARTESIAN_POINT('Origin',(-7.90471375114085E-13,4.8,14.15));
#31598=CARTESIAN_POINT('',(-3.90037061894662E-13,4.2,14.15));
#31599=CARTESIAN_POINT('Ctrl Pts',(1.21301265455545E-14,4.19999999999999,
14.15));
#31600=CARTESIAN_POINT('Ctrl Pts',(-5.86112190757927,4.27499999999999,14.15));
#31601=CARTESIAN_POINT('Ctrl Pts',(-10.0055609537896,4.34999999999999,10.0055609537896));
#31602=CARTESIAN_POINT('Ctrl Pts',(-14.15,4.42499999999999,5.86112190757931));
#31603=CARTESIAN_POINT('Ctrl Pts',(-14.15,4.49999999999999,-1.21388851215623E-14));
#31604=CARTESIAN_POINT('Ctrl Pts',(-14.15,4.57499999999999,-5.86112190757929));
#31605=CARTESIAN_POINT('Ctrl Pts',(-10.0055609537897,4.64999999999999,-10.0055609537896));
#31606=CARTESIAN_POINT('Ctrl Pts',(-5.86112190757929,4.72499999999999,-14.15));
#31607=CARTESIAN_POINT('Ctrl Pts',(-1.3863001766348E-14,4.79999999999999,
-14.15));
#31608=CARTESIAN_POINT('Ctrl Pts',(5.86112190757926,4.87499999999999,-14.15));
#31609=CARTESIAN_POINT('Ctrl Pts',(10.0055609537896,4.94999999999999,-10.0055609537896));
#31610=CARTESIAN_POINT('Ctrl Pts',(14.15,5.02499999999999,-5.86112190757932));
#31611=CARTESIAN_POINT('Ctrl Pts',(14.15,5.09999999999999,-3.98648886542583E-14));
#31612=CARTESIAN_POINT('Ctrl Pts',(14.15,5.17499999999999,5.86112190757929));
#31613=CARTESIAN_POINT('Ctrl Pts',(10.0055609537897,5.24999999999999,10.0055609537896));
#31614=CARTESIAN_POINT('Ctrl Pts',(5.86112190757929,5.32499999999999,14.15));
#31615=CARTESIAN_POINT('Ctrl Pts',(-3.86571311453075E-13,5.39999999999999,
14.15));
#31616=CARTESIAN_POINT('',(1.7328752207935E-15,0.599999999999999,14.15));
#31617=CARTESIAN_POINT('Ctrl Pts',(1.7328752207935E-15,0.599999999999999,
14.15));
#31618=CARTESIAN_POINT('Ctrl Pts',(-5.86112190757929,0.674999999999999,
14.15));
#31619=CARTESIAN_POINT('Ctrl Pts',(-10.0055609537896,0.749999999999998,
10.0055609537896));
#31620=CARTESIAN_POINT('Ctrl Pts',(-14.15,0.824999999999999,5.8611219075793));
#31621=CARTESIAN_POINT('Ctrl Pts',(-14.15,0.899999999999998,2.59931283119026E-15));
#31622=CARTESIAN_POINT('Ctrl Pts',(-14.15,0.974999999999998,-5.86112190757929));
#31623=CARTESIAN_POINT('Ctrl Pts',(-10.0055609537896,1.05,-10.0055609537896));
#31624=CARTESIAN_POINT('Ctrl Pts',(-5.8611219075793,1.125,-14.15));
#31625=CARTESIAN_POINT('Ctrl Pts',(-3.46575044158701E-15,1.2,-14.15));
#31626=CARTESIAN_POINT('Ctrl Pts',(5.86112190757929,1.275,-14.15));
#31627=CARTESIAN_POINT('Ctrl Pts',(10.0055609537896,1.35,-10.0055609537897));
#31628=CARTESIAN_POINT('Ctrl Pts',(14.15,1.425,-5.8611219075793));
#31629=CARTESIAN_POINT('Ctrl Pts',(14.15,1.5,-4.33218805198376E-15));
#31630=CARTESIAN_POINT('Ctrl Pts',(14.15,1.575,5.8611219075793));
#31631=CARTESIAN_POINT('Ctrl Pts',(10.0055609537897,1.65,10.0055609537896));
#31632=CARTESIAN_POINT('Ctrl Pts',(5.86112190757931,1.725,14.15));
#31633=CARTESIAN_POINT('Ctrl Pts',(5.19862566238051E-15,1.8,14.15));
#31634=CARTESIAN_POINT('Ctrl Pts',(-5.8611219075793,1.875,14.15));
#31635=CARTESIAN_POINT('Ctrl Pts',(-10.0055609537896,1.95,10.0055609537897));
#31636=CARTESIAN_POINT('Ctrl Pts',(-14.15,2.025,5.86112190757931));
#31637=CARTESIAN_POINT('Ctrl Pts',(-14.15,2.1,6.06506327277727E-15));
#31638=CARTESIAN_POINT('Ctrl Pts',(-14.15,2.175,-5.8611219075793));
#31639=CARTESIAN_POINT('Ctrl Pts',(-10.0055609537897,2.25,-10.0055609537896));
#31640=CARTESIAN_POINT('Ctrl Pts',(-5.86112190757931,2.32499999999999,-14.15));
#31641=CARTESIAN_POINT('Ctrl Pts',(-6.93150088317402E-15,2.4,-14.15));
#31642=CARTESIAN_POINT('Ctrl Pts',(5.86112190757929,2.475,-14.15));
#31643=CARTESIAN_POINT('Ctrl Pts',(10.0055609537896,2.54999999999999,-10.0055609537896));
#31644=CARTESIAN_POINT('Ctrl Pts',(14.15,2.625,-5.86112190757931));
#31645=CARTESIAN_POINT('Ctrl Pts',(14.15,2.69999999999999,-7.79793849357077E-15));
#31646=CARTESIAN_POINT('Ctrl Pts',(14.15,2.77499999999999,5.86112190757929));
#31647=CARTESIAN_POINT('Ctrl Pts',(10.0055609537897,2.84999999999999,10.0055609537896));
#31648=CARTESIAN_POINT('Ctrl Pts',(5.86112190757931,2.92499999999999,14.15));
#31649=CARTESIAN_POINT('Ctrl Pts',(8.66437610396752E-15,2.99999999999999,
14.15));
#31650=CARTESIAN_POINT('Ctrl Pts',(-5.86112190757929,3.07499999999999,14.15));
#31651=CARTESIAN_POINT('Ctrl Pts',(-10.0055609537896,3.14999999999999,10.0055609537896));
#31652=CARTESIAN_POINT('Ctrl Pts',(-14.15,3.22499999999999,5.86112190757931));
#31653=CARTESIAN_POINT('Ctrl Pts',(-14.15,3.29999999999999,9.53081371436428E-15));
#31654=CARTESIAN_POINT('Ctrl Pts',(-14.15,3.37499999999999,-5.86112190757929));
#31655=CARTESIAN_POINT('Ctrl Pts',(-10.0055609537897,3.44999999999999,-10.0055609537896));
#31656=CARTESIAN_POINT('Ctrl Pts',(-5.86112190757931,3.52499999999999,-14.15));
#31657=CARTESIAN_POINT('Ctrl Pts',(-1.0397251324761E-14,3.59999999999999,
-14.15));
#31658=CARTESIAN_POINT('Ctrl Pts',(5.86112190757927,3.67499999999999,-14.15));
#31659=CARTESIAN_POINT('Ctrl Pts',(10.0055609537896,3.74999999999999,-10.0055609537896));
#31660=CARTESIAN_POINT('Ctrl Pts',(14.15,3.82499999999999,-5.86112190757931));
#31661=CARTESIAN_POINT('Ctrl Pts',(14.15,3.89999999999999,-3.63991382126713E-14));
#31662=CARTESIAN_POINT('Ctrl Pts',(14.15,3.97499999999999,5.86112190757929));
#31663=CARTESIAN_POINT('Ctrl Pts',(10.0055609537897,4.04999999999999,10.0055609537896));
#31664=CARTESIAN_POINT('Ctrl Pts',(5.86112190757929,4.12499999999999,14.15));
#31665=CARTESIAN_POINT('Ctrl Pts',(1.21301265455545E-14,4.19999999999999,
14.15));
#31666=CARTESIAN_POINT('',(0.,0.,13.55));
#31667=CARTESIAN_POINT('Origin',(0.,0.,14.15));
#31668=CARTESIAN_POINT('Ctrl Pts',(0.,0.,13.55));
#31669=CARTESIAN_POINT('Ctrl Pts',(-5.61259377015544,0.0749999999999999,
13.55));
#31670=CARTESIAN_POINT('Ctrl Pts',(-9.58129688507772,0.15,9.58129688507772));
#31671=CARTESIAN_POINT('Ctrl Pts',(-13.55,0.225,5.61259377015544));
#31672=CARTESIAN_POINT('Ctrl Pts',(-13.55,0.299999999999999,8.29698206422332E-16));
#31673=CARTESIAN_POINT('Ctrl Pts',(-13.55,0.374999999999999,-5.61259377015544));
#31674=CARTESIAN_POINT('Ctrl Pts',(-9.58129688507772,0.449999999999999,
-9.58129688507772));
#31675=CARTESIAN_POINT('Ctrl Pts',(-5.61259377015544,0.524999999999999,
-13.55));
#31676=CARTESIAN_POINT('Ctrl Pts',(-1.65939641284466E-15,0.599999999999999,
-13.55));
#31677=CARTESIAN_POINT('Ctrl Pts',(5.61259377015544,0.674999999999998,-13.55));
#31678=CARTESIAN_POINT('Ctrl Pts',(9.58129688507772,0.749999999999998,-9.58129688507772));
#31679=CARTESIAN_POINT('Ctrl Pts',(13.55,0.824999999999998,-5.61259377015545));
#31680=CARTESIAN_POINT('Ctrl Pts',(13.55,0.899999999999998,-2.489094619267E-15));
#31681=CARTESIAN_POINT('Ctrl Pts',(13.55,0.974999999999998,5.61259377015544));
#31682=CARTESIAN_POINT('Ctrl Pts',(9.58129688507772,1.05,9.58129688507772));
#31683=CARTESIAN_POINT('Ctrl Pts',(5.61259377015545,1.125,13.55));
#31684=CARTESIAN_POINT('Ctrl Pts',(3.31879282568933E-15,1.2,13.55));
#31685=CARTESIAN_POINT('Ctrl Pts',(-5.61259377015544,1.275,13.55));
#31686=CARTESIAN_POINT('Ctrl Pts',(-9.58129688507772,1.35,9.58129688507772));
#31687=CARTESIAN_POINT('Ctrl Pts',(-13.55,1.425,5.61259377015545));
#31688=CARTESIAN_POINT('Ctrl Pts',(-13.55,1.5,4.14849103211166E-15));
#31689=CARTESIAN_POINT('Ctrl Pts',(-13.55,1.575,-5.61259377015544));
#31690=CARTESIAN_POINT('Ctrl Pts',(-9.58129688507773,1.65,-9.58129688507771));
#31691=CARTESIAN_POINT('Ctrl Pts',(-5.61259377015545,1.725,-13.55));
#31692=CARTESIAN_POINT('Ctrl Pts',(-4.97818923853399E-15,1.8,-13.55));
#31693=CARTESIAN_POINT('Ctrl Pts',(5.61259377015544,1.875,-13.55));
#31694=CARTESIAN_POINT('Ctrl Pts',(9.58129688507773,1.95,-9.58129688507771));
#31695=CARTESIAN_POINT('Ctrl Pts',(13.55,2.025,-5.61259377015545));
#31696=CARTESIAN_POINT('Ctrl Pts',(13.55,2.1,-5.80788744495632E-15));
#31697=CARTESIAN_POINT('Ctrl Pts',(13.55,2.17499999999999,5.61259377015544));
#31698=CARTESIAN_POINT('Ctrl Pts',(9.58129688507773,2.25,9.58129688507771));
#31699=CARTESIAN_POINT('Ctrl Pts',(5.61259377015545,2.32499999999999,13.55));
#31700=CARTESIAN_POINT('Ctrl Pts',(6.63758565137865E-15,2.39999999999999,
13.55));
#31701=CARTESIAN_POINT('Ctrl Pts',(-5.61259377015544,2.475,13.55));
#31702=CARTESIAN_POINT('Ctrl Pts',(-9.58129688507772,2.54999999999999,9.58129688507772));
#31703=CARTESIAN_POINT('Ctrl Pts',(-13.55,2.62499999999999,5.61259377015545));
#31704=CARTESIAN_POINT('Ctrl Pts',(-13.55,2.69999999999999,7.46728385780099E-15));
#31705=CARTESIAN_POINT('Ctrl Pts',(-13.55,2.77499999999999,-5.61259377015544));
#31706=CARTESIAN_POINT('Ctrl Pts',(-9.58129688507773,2.84999999999999,-9.5812968850777));
#31707=CARTESIAN_POINT('Ctrl Pts',(-5.61259377015545,2.92499999999999,-13.55));
#31708=CARTESIAN_POINT('Ctrl Pts',(-8.29698206422332E-15,2.99999999999999,
-13.55));
#31709=CARTESIAN_POINT('Ctrl Pts',(5.61259377015541,3.07499999999999,-13.55));
#31710=CARTESIAN_POINT('Ctrl Pts',(9.58129688507772,3.14999999999999,-9.58129688507772));
#31711=CARTESIAN_POINT('Ctrl Pts',(13.55,3.22499999999999,-5.61259377015545));
#31712=CARTESIAN_POINT('Ctrl Pts',(13.55,3.29999999999999,-3.3196315444519E-14));
#31713=CARTESIAN_POINT('Ctrl Pts',(13.55,3.37499999999999,5.61259377015544));
#31714=CARTESIAN_POINT('Ctrl Pts',(9.58129688507773,3.44999999999999,9.5812968850777));
#31715=CARTESIAN_POINT('Ctrl Pts',(5.61259377015543,3.52499999999999,13.55));
#31716=CARTESIAN_POINT('Ctrl Pts',(9.95637847706798E-15,3.59999999999999,
13.55));
#31717=CARTESIAN_POINT('Ctrl Pts',(-5.61259377015541,3.67499999999999,13.55));
#31718=CARTESIAN_POINT('Ctrl Pts',(-9.58129688507772,3.74999999999999,9.58129688507772));
#31719=CARTESIAN_POINT('Ctrl Pts',(-13.55,3.82499999999999,5.61259377015546));
#31720=CARTESIAN_POINT('Ctrl Pts',(-13.55,3.89999999999999,-1.32835584903831E-14));
#31721=CARTESIAN_POINT('Ctrl Pts',(-13.55,3.97499999999999,-5.61259377015543));
#31722=CARTESIAN_POINT('Ctrl Pts',(-9.58129688507774,4.04999999999999,-9.5812968850777));
#31723=CARTESIAN_POINT('Ctrl Pts',(-5.61259377015543,4.12499999999999,-13.55));
#31724=CARTESIAN_POINT('Ctrl Pts',(-1.16157748899126E-14,4.19999999999999,
-13.55));
#31725=CARTESIAN_POINT('Ctrl Pts',(5.61259377015541,4.27499999999999,-13.55));
#31726=CARTESIAN_POINT('Ctrl Pts',(9.58129688507772,4.34999999999999,-9.58129688507772));
#31727=CARTESIAN_POINT('Ctrl Pts',(13.55,4.42499999999999,-5.61259377015546));
#31728=CARTESIAN_POINT('Ctrl Pts',(13.55,4.49999999999999,-3.65151082702084E-14));
#31729=CARTESIAN_POINT('Ctrl Pts',(13.55,4.57499999999999,5.61259377015543));
#31730=CARTESIAN_POINT('Ctrl Pts',(9.58129688507774,4.64999999999999,9.5812968850777));
#31731=CARTESIAN_POINT('Ctrl Pts',(5.61259377015543,4.72499999999999,13.55));
#31732=CARTESIAN_POINT('Ctrl Pts',(-3.71838991479217E-13,4.79999999999999,
13.55));
#31733=CARTESIAN_POINT('Ctrl Pts',(0.,-0.6,14.15));
#31734=CARTESIAN_POINT('Ctrl Pts',(-5.8611219075793,-0.525,14.15));
#31735=CARTESIAN_POINT('Ctrl Pts',(-10.0055609537896,-0.450000000000001,
10.0055609537896));
#31736=CARTESIAN_POINT('Ctrl Pts',(-14.15,-0.375000000000001,5.8611219075793));
#31737=CARTESIAN_POINT('Ctrl Pts',(-14.15,-0.300000000000001,8.66437610396752E-16));
#31738=CARTESIAN_POINT('Ctrl Pts',(-14.15,-0.225000000000001,-5.86112190757929));
#31739=CARTESIAN_POINT('Ctrl Pts',(-10.0055609537896,-0.150000000000001,
-10.0055609537896));
#31740=CARTESIAN_POINT('Ctrl Pts',(-5.8611219075793,-0.0750000000000014,
-14.15));
#31741=CARTESIAN_POINT('Ctrl Pts',(-1.7328752207935E-15,-1.51788304147971E-15,
-14.15));
#31742=CARTESIAN_POINT('Ctrl Pts',(5.86112190757929,0.0749999999999984,
-14.15));
#31743=CARTESIAN_POINT('Ctrl Pts',(10.0055609537896,0.149999999999998,-10.0055609537896));
#31744=CARTESIAN_POINT('Ctrl Pts',(14.15,0.224999999999998,-5.8611219075793));
#31745=CARTESIAN_POINT('Ctrl Pts',(14.15,0.299999999999998,-2.59931283119026E-15));
#31746=CARTESIAN_POINT('Ctrl Pts',(14.15,0.374999999999998,5.8611219075793));
#31747=CARTESIAN_POINT('Ctrl Pts',(10.0055609537896,0.449999999999997,10.0055609537896));
#31748=CARTESIAN_POINT('Ctrl Pts',(5.8611219075793,0.524999999999997,14.15));
#31749=CARTESIAN_POINT('Ctrl Pts',(0.,0.599999999999997,14.15));
#31750=CARTESIAN_POINT('Ctrl Pts',(-5.8611219075793,0.674999999999997,14.15));
#31751=CARTESIAN_POINT('Ctrl Pts',(-10.0055609537896,0.749999999999997,
10.0055609537896));
#31752=CARTESIAN_POINT('Ctrl Pts',(-14.15,0.824999999999997,5.8611219075793));
#31753=CARTESIAN_POINT('Ctrl Pts',(-14.15,0.899999999999996,8.66437610396752E-16));
#31754=CARTESIAN_POINT('Ctrl Pts',(-14.15,0.974999999999996,-5.86112190757929));
#31755=CARTESIAN_POINT('Ctrl Pts',(-10.0055609537896,1.05,-10.0055609537896));
#31756=CARTESIAN_POINT('Ctrl Pts',(-5.8611219075793,1.125,-14.15));
#31757=CARTESIAN_POINT('Ctrl Pts',(-1.7328752207935E-15,1.2,-14.15));
#31758=CARTESIAN_POINT('Ctrl Pts',(5.86112190757929,1.275,-14.15));
#31759=CARTESIAN_POINT('Ctrl Pts',(10.0055609537896,1.35,-10.0055609537896));
#31760=CARTESIAN_POINT('Ctrl Pts',(14.15,1.425,-5.8611219075793));
#31761=CARTESIAN_POINT('Ctrl Pts',(14.15,1.49999999999999,-2.59931283119026E-15));
#31762=CARTESIAN_POINT('Ctrl Pts',(14.15,1.57499999999999,5.8611219075793));
#31763=CARTESIAN_POINT('Ctrl Pts',(10.0055609537896,1.64999999999999,10.0055609537896));
#31764=CARTESIAN_POINT('Ctrl Pts',(5.8611219075793,1.72499999999999,14.15));
#31765=CARTESIAN_POINT('Ctrl Pts',(0.,1.79999999999999,14.15));
#31766=CARTESIAN_POINT('Ctrl Pts',(-5.8611219075793,1.87499999999999,14.15));
#31767=CARTESIAN_POINT('Ctrl Pts',(-10.0055609537896,1.94999999999999,10.0055609537896));
#31768=CARTESIAN_POINT('Ctrl Pts',(-14.15,2.02499999999999,5.8611219075793));
#31769=CARTESIAN_POINT('Ctrl Pts',(-14.15,2.09999999999999,8.66437610396752E-16));
#31770=CARTESIAN_POINT('Ctrl Pts',(-14.15,2.17499999999999,-5.86112190757929));
#31771=CARTESIAN_POINT('Ctrl Pts',(-10.0055609537896,2.24999999999999,-10.0055609537896));
#31772=CARTESIAN_POINT('Ctrl Pts',(-5.8611219075793,2.32499999999999,-14.15));
#31773=CARTESIAN_POINT('Ctrl Pts',(-1.7328752207935E-15,2.39999999999999,
-14.15));
#31774=CARTESIAN_POINT('Ctrl Pts',(5.86112190757929,2.47499999999999,-14.15));
#31775=CARTESIAN_POINT('Ctrl Pts',(10.0055609537896,2.54999999999999,-10.0055609537896));
#31776=CARTESIAN_POINT('Ctrl Pts',(14.15,2.62499999999999,-5.8611219075793));
#31777=CARTESIAN_POINT('Ctrl Pts',(14.15,2.69999999999999,-2.59931283119026E-15));
#31778=CARTESIAN_POINT('Ctrl Pts',(14.15,2.77499999999999,5.8611219075793));
#31779=CARTESIAN_POINT('Ctrl Pts',(10.0055609537896,2.84999999999999,10.0055609537896));
#31780=CARTESIAN_POINT('Ctrl Pts',(5.8611219075793,2.92499999999999,14.15));
#31781=CARTESIAN_POINT('Ctrl Pts',(0.,2.99999999999999,14.15));
#31782=CARTESIAN_POINT('Ctrl Pts',(-5.8611219075793,3.07499999999999,14.15));
#31783=CARTESIAN_POINT('Ctrl Pts',(-10.0055609537896,3.14999999999999,10.0055609537896));
#31784=CARTESIAN_POINT('Ctrl Pts',(-14.15,3.22499999999999,5.8611219075793));
#31785=CARTESIAN_POINT('Ctrl Pts',(-14.15,3.29999999999999,8.66437610396752E-16));
#31786=CARTESIAN_POINT('Ctrl Pts',(-14.15,3.37499999999999,-5.86112190757929));
#31787=CARTESIAN_POINT('Ctrl Pts',(-10.0055609537896,3.44999999999999,-10.0055609537896));
#31788=CARTESIAN_POINT('Ctrl Pts',(-5.8611219075793,3.52499999999999,-14.15));
#31789=CARTESIAN_POINT('Ctrl Pts',(-1.7328752207935E-15,3.59999999999999,
-14.15));
#31790=CARTESIAN_POINT('Ctrl Pts',(5.86112190757929,3.67499999999999,-14.15));
#31791=CARTESIAN_POINT('Ctrl Pts',(10.0055609537896,3.74999999999999,-10.0055609537896));
#31792=CARTESIAN_POINT('Ctrl Pts',(14.15,3.82499999999999,-5.8611219075793));
#31793=CARTESIAN_POINT('Ctrl Pts',(14.15,3.89999999999999,-2.59931283119026E-15));
#31794=CARTESIAN_POINT('Ctrl Pts',(14.15,3.97499999999999,5.8611219075793));
#31795=CARTESIAN_POINT('Ctrl Pts',(10.0055609537896,4.04999999999999,10.0055609537896));
#31796=CARTESIAN_POINT('Ctrl Pts',(5.8611219075793,4.12499999999999,14.15));
#31797=CARTESIAN_POINT('Ctrl Pts',(0.,4.19999999999999,14.15));
#31798=CARTESIAN_POINT('Ctrl Pts',(0.,-0.6,13.7985281374239));
#31799=CARTESIAN_POINT('Ctrl Pts',(-5.71553749530772,-0.525,13.7985281374239));
#31800=CARTESIAN_POINT('Ctrl Pts',(-9.75703281636579,-0.450000000000001,
9.75703281636579));
#31801=CARTESIAN_POINT('Ctrl Pts',(-13.7985281374239,-0.375000000000001,
5.71553749530772));
#31802=CARTESIAN_POINT('Ctrl Pts',(-13.7985281374239,-0.300000000000001,
8.44916165822041E-16));
#31803=CARTESIAN_POINT('Ctrl Pts',(-13.7985281374239,-0.225000000000001,
-5.71553749530772));
#31804=CARTESIAN_POINT('Ctrl Pts',(-9.75703281636579,-0.150000000000001,
-9.75703281636579));
#31805=CARTESIAN_POINT('Ctrl Pts',(-5.71553749530773,-0.0750000000000015,
-13.7985281374239));
#31806=CARTESIAN_POINT('Ctrl Pts',(-1.68983233164408E-15,-1.62630325872826E-15,
-13.7985281374239));
#31807=CARTESIAN_POINT('Ctrl Pts',(5.71553749530772,0.0749999999999982,
-13.7985281374239));
#31808=CARTESIAN_POINT('Ctrl Pts',(9.75703281636579,0.149999999999998,-9.75703281636579));
#31809=CARTESIAN_POINT('Ctrl Pts',(13.7985281374239,0.224999999999998,-5.71553749530773));
#31810=CARTESIAN_POINT('Ctrl Pts',(13.7985281374239,0.299999999999998,-2.53474849746612E-15));
#31811=CARTESIAN_POINT('Ctrl Pts',(13.7985281374239,0.374999999999998,5.71553749530773));
#31812=CARTESIAN_POINT('Ctrl Pts',(9.75703281636579,0.449999999999997,9.75703281636579));
#31813=CARTESIAN_POINT('Ctrl Pts',(5.71553749530774,0.524999999999997,13.7985281374239));
#31814=CARTESIAN_POINT('Ctrl Pts',(0.,0.599999999999997,13.7985281374239));
#31815=CARTESIAN_POINT('Ctrl Pts',(-5.71553749530772,0.674999999999997,
13.7985281374239));
#31816=CARTESIAN_POINT('Ctrl Pts',(-9.75703281636579,0.749999999999997,
9.75703281636579));
#31817=CARTESIAN_POINT('Ctrl Pts',(-13.7985281374239,0.824999999999997,
5.71553749530772));
#31818=CARTESIAN_POINT('Ctrl Pts',(-13.7985281374239,0.899999999999996,
8.44916165822041E-16));
#31819=CARTESIAN_POINT('Ctrl Pts',(-13.7985281374239,0.974999999999996,
-5.71553749530772));
#31820=CARTESIAN_POINT('Ctrl Pts',(-9.75703281636579,1.05,-9.75703281636579));
#31821=CARTESIAN_POINT('Ctrl Pts',(-5.71553749530773,1.125,-13.7985281374239));
#31822=CARTESIAN_POINT('Ctrl Pts',(-1.68983233164408E-15,1.2,-13.7985281374239));
#31823=CARTESIAN_POINT('Ctrl Pts',(5.71553749530772,1.275,-13.7985281374239));
#31824=CARTESIAN_POINT('Ctrl Pts',(9.75703281636579,1.35,-9.75703281636579));
#31825=CARTESIAN_POINT('Ctrl Pts',(13.7985281374239,1.425,-5.71553749530773));
#31826=CARTESIAN_POINT('Ctrl Pts',(13.7985281374239,1.49999999999999,-2.53474849746612E-15));
#31827=CARTESIAN_POINT('Ctrl Pts',(13.7985281374239,1.57499999999999,5.71553749530773));
#31828=CARTESIAN_POINT('Ctrl Pts',(9.75703281636579,1.65,9.75703281636579));
#31829=CARTESIAN_POINT('Ctrl Pts',(5.71553749530774,1.72499999999999,13.7985281374239));
#31830=CARTESIAN_POINT('Ctrl Pts',(0.,1.79999999999999,13.7985281374239));
#31831=CARTESIAN_POINT('Ctrl Pts',(-5.71553749530772,1.87499999999999,13.7985281374239));
#31832=CARTESIAN_POINT('Ctrl Pts',(-9.75703281636579,1.94999999999999,9.75703281636579));
#31833=CARTESIAN_POINT('Ctrl Pts',(-13.7985281374239,2.02499999999999,5.71553749530772));
#31834=CARTESIAN_POINT('Ctrl Pts',(-13.7985281374239,2.09999999999999,8.44916165822041E-16));
#31835=CARTESIAN_POINT('Ctrl Pts',(-13.7985281374239,2.17499999999999,-5.71553749530772));
#31836=CARTESIAN_POINT('Ctrl Pts',(-9.75703281636579,2.24999999999999,-9.75703281636579));
#31837=CARTESIAN_POINT('Ctrl Pts',(-5.71553749530773,2.32499999999999,-13.7985281374239));
#31838=CARTESIAN_POINT('Ctrl Pts',(-1.68983233164408E-15,2.39999999999999,
-13.7985281374239));
#31839=CARTESIAN_POINT('Ctrl Pts',(5.71553749530772,2.47499999999999,-13.7985281374239));
#31840=CARTESIAN_POINT('Ctrl Pts',(9.75703281636579,2.54999999999999,-9.75703281636579));
#31841=CARTESIAN_POINT('Ctrl Pts',(13.7985281374239,2.62499999999999,-5.71553749530773));
#31842=CARTESIAN_POINT('Ctrl Pts',(13.7985281374239,2.69999999999999,-2.53474849746612E-15));
#31843=CARTESIAN_POINT('Ctrl Pts',(13.7985281374239,2.77499999999999,5.71553749530773));
#31844=CARTESIAN_POINT('Ctrl Pts',(9.75703281636579,2.84999999999999,9.75703281636579));
#31845=CARTESIAN_POINT('Ctrl Pts',(5.71553749530774,2.92499999999999,13.7985281374239));
#31846=CARTESIAN_POINT('Ctrl Pts',(0.,2.99999999999999,13.7985281374239));
#31847=CARTESIAN_POINT('Ctrl Pts',(-5.71553749530772,3.07499999999999,13.7985281374239));
#31848=CARTESIAN_POINT('Ctrl Pts',(-9.75703281636579,3.14999999999999,9.75703281636579));
#31849=CARTESIAN_POINT('Ctrl Pts',(-13.7985281374239,3.22499999999999,5.71553749530772));
#31850=CARTESIAN_POINT('Ctrl Pts',(-13.7985281374239,3.29999999999999,8.44916165822041E-16));
#31851=CARTESIAN_POINT('Ctrl Pts',(-13.7985281374239,3.37499999999999,-5.71553749530772));
#31852=CARTESIAN_POINT('Ctrl Pts',(-9.75703281636579,3.44999999999999,-9.75703281636579));
#31853=CARTESIAN_POINT('Ctrl Pts',(-5.71553749530773,3.52499999999999,-13.7985281374239));
#31854=CARTESIAN_POINT('Ctrl Pts',(-1.68983233164408E-15,3.59999999999999,
-13.7985281374239));
#31855=CARTESIAN_POINT('Ctrl Pts',(5.71553749530772,3.67499999999999,-13.7985281374239));
#31856=CARTESIAN_POINT('Ctrl Pts',(9.75703281636579,3.74999999999999,-9.75703281636579));
#31857=CARTESIAN_POINT('Ctrl Pts',(13.7985281374239,3.82499999999999,-5.71553749530773));
#31858=CARTESIAN_POINT('Ctrl Pts',(13.7985281374239,3.89999999999999,-2.53474849746612E-15));
#31859=CARTESIAN_POINT('Ctrl Pts',(13.7985281374239,3.97499999999999,5.71553749530773));
#31860=CARTESIAN_POINT('Ctrl Pts',(9.75703281636579,4.04999999999999,9.75703281636579));
#31861=CARTESIAN_POINT('Ctrl Pts',(5.71553749530774,4.12499999999999,13.7985281374239));
#31862=CARTESIAN_POINT('Ctrl Pts',(0.,4.19999999999999,13.7985281374239));
#31863=CARTESIAN_POINT('Ctrl Pts',(0.,-0.351471862576143,13.55));
#31864=CARTESIAN_POINT('Ctrl Pts',(-5.61259377015544,-0.276471862576143,
13.55));
#31865=CARTESIAN_POINT('Ctrl Pts',(-9.58129688507772,-0.201471862576143,
9.58129688507772));
#31866=CARTESIAN_POINT('Ctrl Pts',(-13.55,-0.126471862576144,5.61259377015544));
#31867=CARTESIAN_POINT('Ctrl Pts',(-13.55,-0.0514718625761438,8.29698206422332E-16));
#31868=CARTESIAN_POINT('Ctrl Pts',(-13.55,0.0235281374238561,-5.61259377015544));
#31869=CARTESIAN_POINT('Ctrl Pts',(-9.58129688507772,0.098528137423856,
-9.58129688507772));
#31870=CARTESIAN_POINT('Ctrl Pts',(-5.61259377015544,0.173528137423856,
-13.55));
#31871=CARTESIAN_POINT('Ctrl Pts',(-1.65939641284466E-15,0.248528137423856,
-13.55));
#31872=CARTESIAN_POINT('Ctrl Pts',(5.61259377015544,0.323528137423855,-13.55));
#31873=CARTESIAN_POINT('Ctrl Pts',(9.58129688507772,0.398528137423855,-9.58129688507772));
#31874=CARTESIAN_POINT('Ctrl Pts',(13.55,0.473528137423855,-5.61259377015545));
#31875=CARTESIAN_POINT('Ctrl Pts',(13.55,0.548528137423855,-2.489094619267E-15));
#31876=CARTESIAN_POINT('Ctrl Pts',(13.55,0.623528137423855,5.61259377015544));
#31877=CARTESIAN_POINT('Ctrl Pts',(9.58129688507772,0.698528137423855,9.58129688507772));
#31878=CARTESIAN_POINT('Ctrl Pts',(5.61259377015545,0.773528137423855,13.55));
#31879=CARTESIAN_POINT('Ctrl Pts',(0.,0.848528137423854,13.55));
#31880=CARTESIAN_POINT('Ctrl Pts',(-5.61259377015544,0.923528137423854,
13.55));
#31881=CARTESIAN_POINT('Ctrl Pts',(-9.58129688507772,0.998528137423854,
9.58129688507772));
#31882=CARTESIAN_POINT('Ctrl Pts',(-13.55,1.07352813742385,5.61259377015544));
#31883=CARTESIAN_POINT('Ctrl Pts',(-13.55,1.14852813742385,8.29698206422332E-16));
#31884=CARTESIAN_POINT('Ctrl Pts',(-13.55,1.22352813742385,-5.61259377015544));
#31885=CARTESIAN_POINT('Ctrl Pts',(-9.58129688507772,1.29852813742385,-9.58129688507772));
#31886=CARTESIAN_POINT('Ctrl Pts',(-5.61259377015544,1.37352813742385,-13.55));
#31887=CARTESIAN_POINT('Ctrl Pts',(-1.65939641284466E-15,1.44852813742385,
-13.55));
#31888=CARTESIAN_POINT('Ctrl Pts',(5.61259377015544,1.52352813742385,-13.55));
#31889=CARTESIAN_POINT('Ctrl Pts',(9.58129688507772,1.59852813742385,-9.58129688507772));
#31890=CARTESIAN_POINT('Ctrl Pts',(13.55,1.67352813742385,-5.61259377015545));
#31891=CARTESIAN_POINT('Ctrl Pts',(13.55,1.74852813742385,-2.489094619267E-15));
#31892=CARTESIAN_POINT('Ctrl Pts',(13.55,1.82352813742385,5.61259377015544));
#31893=CARTESIAN_POINT('Ctrl Pts',(9.58129688507772,1.89852813742385,9.58129688507772));
#31894=CARTESIAN_POINT('Ctrl Pts',(5.61259377015545,1.97352813742385,13.55));
#31895=CARTESIAN_POINT('Ctrl Pts',(0.,2.04852813742385,13.55));
#31896=CARTESIAN_POINT('Ctrl Pts',(-5.61259377015544,2.12352813742385,13.55));
#31897=CARTESIAN_POINT('Ctrl Pts',(-9.58129688507772,2.19852813742385,9.58129688507772));
#31898=CARTESIAN_POINT('Ctrl Pts',(-13.55,2.27352813742385,5.61259377015544));
#31899=CARTESIAN_POINT('Ctrl Pts',(-13.55,2.34852813742385,8.29698206422332E-16));
#31900=CARTESIAN_POINT('Ctrl Pts',(-13.55,2.42352813742385,-5.61259377015544));
#31901=CARTESIAN_POINT('Ctrl Pts',(-9.58129688507772,2.49852813742385,-9.58129688507772));
#31902=CARTESIAN_POINT('Ctrl Pts',(-5.61259377015544,2.57352813742385,-13.55));
#31903=CARTESIAN_POINT('Ctrl Pts',(-1.65939641284466E-15,2.64852813742385,
-13.55));
#31904=CARTESIAN_POINT('Ctrl Pts',(5.61259377015544,2.72352813742385,-13.55));
#31905=CARTESIAN_POINT('Ctrl Pts',(9.58129688507772,2.79852813742385,-9.58129688507772));
#31906=CARTESIAN_POINT('Ctrl Pts',(13.55,2.87352813742385,-5.61259377015545));
#31907=CARTESIAN_POINT('Ctrl Pts',(13.55,2.94852813742385,-2.489094619267E-15));
#31908=CARTESIAN_POINT('Ctrl Pts',(13.55,3.02352813742385,5.61259377015544));
#31909=CARTESIAN_POINT('Ctrl Pts',(9.58129688507772,3.09852813742385,9.58129688507772));
#31910=CARTESIAN_POINT('Ctrl Pts',(5.61259377015545,3.17352813742385,13.55));
#31911=CARTESIAN_POINT('Ctrl Pts',(0.,3.24852813742385,13.55));
#31912=CARTESIAN_POINT('Ctrl Pts',(-5.61259377015544,3.32352813742385,13.55));
#31913=CARTESIAN_POINT('Ctrl Pts',(-9.58129688507772,3.39852813742385,9.58129688507772));
#31914=CARTESIAN_POINT('Ctrl Pts',(-13.55,3.47352813742385,5.61259377015544));
#31915=CARTESIAN_POINT('Ctrl Pts',(-13.55,3.54852813742385,8.29698206422332E-16));
#31916=CARTESIAN_POINT('Ctrl Pts',(-13.55,3.62352813742385,-5.61259377015544));
#31917=CARTESIAN_POINT('Ctrl Pts',(-9.58129688507772,3.69852813742385,-9.58129688507772));
#31918=CARTESIAN_POINT('Ctrl Pts',(-5.61259377015544,3.77352813742385,-13.55));
#31919=CARTESIAN_POINT('Ctrl Pts',(-1.65939641284466E-15,3.84852813742385,
-13.55));
#31920=CARTESIAN_POINT('Ctrl Pts',(5.61259377015544,3.92352813742385,-13.55));
#31921=CARTESIAN_POINT('Ctrl Pts',(9.58129688507772,3.99852813742385,-9.58129688507772));
#31922=CARTESIAN_POINT('Ctrl Pts',(13.55,4.07352813742385,-5.61259377015545));
#31923=CARTESIAN_POINT('Ctrl Pts',(13.55,4.14852813742385,-2.489094619267E-15));
#31924=CARTESIAN_POINT('Ctrl Pts',(13.55,4.22352813742385,5.61259377015544));
#31925=CARTESIAN_POINT('Ctrl Pts',(9.58129688507772,4.29852813742385,9.58129688507772));
#31926=CARTESIAN_POINT('Ctrl Pts',(5.61259377015545,4.37352813742385,13.55));
#31927=CARTESIAN_POINT('Ctrl Pts',(0.,4.44852813742385,13.55));
#31928=CARTESIAN_POINT('Ctrl Pts',(0.,0.,13.55));
#31929=CARTESIAN_POINT('Ctrl Pts',(-5.61259377015544,0.0749999999999998,
13.55));
#31930=CARTESIAN_POINT('Ctrl Pts',(-9.58129688507772,0.15,9.58129688507772));
#31931=CARTESIAN_POINT('Ctrl Pts',(-13.55,0.225,5.61259377015544));
#31932=CARTESIAN_POINT('Ctrl Pts',(-13.55,0.299999999999999,8.29698206422332E-16));
#31933=CARTESIAN_POINT('Ctrl Pts',(-13.55,0.374999999999999,-5.61259377015544));
#31934=CARTESIAN_POINT('Ctrl Pts',(-9.58129688507772,0.449999999999999,
-9.58129688507772));
#31935=CARTESIAN_POINT('Ctrl Pts',(-5.61259377015544,0.524999999999999,
-13.55));
#31936=CARTESIAN_POINT('Ctrl Pts',(-1.65939641284466E-15,0.599999999999999,
-13.55));
#31937=CARTESIAN_POINT('Ctrl Pts',(5.61259377015543,0.674999999999998,-13.55));
#31938=CARTESIAN_POINT('Ctrl Pts',(9.58129688507772,0.749999999999998,-9.58129688507772));
#31939=CARTESIAN_POINT('Ctrl Pts',(13.55,0.824999999999998,-5.61259377015545));
#31940=CARTESIAN_POINT('Ctrl Pts',(13.55,0.899999999999998,-2.489094619267E-15));
#31941=CARTESIAN_POINT('Ctrl Pts',(13.55,0.974999999999998,5.61259377015544));
#31942=CARTESIAN_POINT('Ctrl Pts',(9.58129688507772,1.05,9.58129688507772));
#31943=CARTESIAN_POINT('Ctrl Pts',(5.61259377015545,1.125,13.55));
#31944=CARTESIAN_POINT('Ctrl Pts',(0.,1.2,13.55));
#31945=CARTESIAN_POINT('Ctrl Pts',(-5.61259377015544,1.275,13.55));
#31946=CARTESIAN_POINT('Ctrl Pts',(-9.58129688507772,1.35,9.58129688507772));
#31947=CARTESIAN_POINT('Ctrl Pts',(-13.55,1.425,5.61259377015544));
#31948=CARTESIAN_POINT('Ctrl Pts',(-13.55,1.5,8.29698206422332E-16));
#31949=CARTESIAN_POINT('Ctrl Pts',(-13.55,1.575,-5.61259377015544));
#31950=CARTESIAN_POINT('Ctrl Pts',(-9.58129688507772,1.65,-9.58129688507772));
#31951=CARTESIAN_POINT('Ctrl Pts',(-5.61259377015544,1.725,-13.55));
#31952=CARTESIAN_POINT('Ctrl Pts',(-1.65939641284466E-15,1.8,-13.55));
#31953=CARTESIAN_POINT('Ctrl Pts',(5.61259377015543,1.875,-13.55));
#31954=CARTESIAN_POINT('Ctrl Pts',(9.58129688507772,1.95,-9.58129688507772));
#31955=CARTESIAN_POINT('Ctrl Pts',(13.55,2.025,-5.61259377015545));
#31956=CARTESIAN_POINT('Ctrl Pts',(13.55,2.1,-2.489094619267E-15));
#31957=CARTESIAN_POINT('Ctrl Pts',(13.55,2.17499999999999,5.61259377015544));
#31958=CARTESIAN_POINT('Ctrl Pts',(9.58129688507772,2.25,9.58129688507772));
#31959=CARTESIAN_POINT('Ctrl Pts',(5.61259377015545,2.32499999999999,13.55));
#31960=CARTESIAN_POINT('Ctrl Pts',(0.,2.39999999999999,13.55));
#31961=CARTESIAN_POINT('Ctrl Pts',(-5.61259377015544,2.47499999999999,13.55));
#31962=CARTESIAN_POINT('Ctrl Pts',(-9.58129688507772,2.54999999999999,9.58129688507772));
#31963=CARTESIAN_POINT('Ctrl Pts',(-13.55,2.62499999999999,5.61259377015544));
#31964=CARTESIAN_POINT('Ctrl Pts',(-13.55,2.69999999999999,8.29698206422332E-16));
#31965=CARTESIAN_POINT('Ctrl Pts',(-13.55,2.77499999999999,-5.61259377015544));
#31966=CARTESIAN_POINT('Ctrl Pts',(-9.58129688507772,2.84999999999999,-9.58129688507772));
#31967=CARTESIAN_POINT('Ctrl Pts',(-5.61259377015544,2.92499999999999,-13.55));
#31968=CARTESIAN_POINT('Ctrl Pts',(-1.65939641284466E-15,2.99999999999999,
-13.55));
#31969=CARTESIAN_POINT('Ctrl Pts',(5.61259377015543,3.07499999999999,-13.55));
#31970=CARTESIAN_POINT('Ctrl Pts',(9.58129688507772,3.14999999999999,-9.58129688507772));
#31971=CARTESIAN_POINT('Ctrl Pts',(13.55,3.22499999999999,-5.61259377015545));
#31972=CARTESIAN_POINT('Ctrl Pts',(13.55,3.29999999999999,-2.489094619267E-15));
#31973=CARTESIAN_POINT('Ctrl Pts',(13.55,3.37499999999999,5.61259377015544));
#31974=CARTESIAN_POINT('Ctrl Pts',(9.58129688507772,3.44999999999999,9.58129688507772));
#31975=CARTESIAN_POINT('Ctrl Pts',(5.61259377015545,3.52499999999999,13.55));
#31976=CARTESIAN_POINT('Ctrl Pts',(0.,3.59999999999999,13.55));
#31977=CARTESIAN_POINT('Ctrl Pts',(-5.61259377015544,3.67499999999999,13.55));
#31978=CARTESIAN_POINT('Ctrl Pts',(-9.58129688507772,3.74999999999999,9.58129688507772));
#31979=CARTESIAN_POINT('Ctrl Pts',(-13.55,3.82499999999999,5.61259377015544));
#31980=CARTESIAN_POINT('Ctrl Pts',(-13.55,3.89999999999999,8.29698206422332E-16));
#31981=CARTESIAN_POINT('Ctrl Pts',(-13.55,3.97499999999999,-5.61259377015544));
#31982=CARTESIAN_POINT('Ctrl Pts',(-9.58129688507772,4.04999999999999,-9.58129688507772));
#31983=CARTESIAN_POINT('Ctrl Pts',(-5.61259377015544,4.12499999999999,-13.55));
#31984=CARTESIAN_POINT('Ctrl Pts',(-1.65939641284466E-15,4.19999999999999,
-13.55));
#31985=CARTESIAN_POINT('Ctrl Pts',(5.61259377015543,4.27499999999999,-13.55));
#31986=CARTESIAN_POINT('Ctrl Pts',(9.58129688507772,4.34999999999999,-9.58129688507772));
#31987=CARTESIAN_POINT('Ctrl Pts',(13.55,4.42499999999999,-5.61259377015545));
#31988=CARTESIAN_POINT('Ctrl Pts',(13.55,4.49999999999999,-2.489094619267E-15));
#31989=CARTESIAN_POINT('Ctrl Pts',(13.55,4.57499999999999,5.61259377015544));
#31990=CARTESIAN_POINT('Ctrl Pts',(9.58129688507772,4.64999999999999,9.58129688507772));
#31991=CARTESIAN_POINT('Ctrl Pts',(5.61259377015545,4.72499999999999,13.55));
#31992=CARTESIAN_POINT('Ctrl Pts',(0.,4.79999999999999,13.55));
#31993=CARTESIAN_POINT('',(-1.7328752207935E-15,-0.599999999999999,14.15));
#31994=CARTESIAN_POINT('Origin',(0.,0.,14.15));
#31995=CARTESIAN_POINT('Ctrl Pts',(-1.7328752207935E-15,-0.599999999999999,
14.15));
#31996=CARTESIAN_POINT('Ctrl Pts',(-5.8611219075793,-0.524999999999999,
14.15));
#31997=CARTESIAN_POINT('Ctrl Pts',(-10.0055609537896,-0.449999999999999,
10.0055609537896));
#31998=CARTESIAN_POINT('Ctrl Pts',(-14.15,-0.374999999999999,5.86112190757929));
#31999=CARTESIAN_POINT('Ctrl Pts',(-14.15,-0.299999999999999,-8.66437610396752E-16));
#32000=CARTESIAN_POINT('Ctrl Pts',(-14.15,-0.225,-5.8611219075793));
#32001=CARTESIAN_POINT('Ctrl Pts',(-10.0055609537896,-0.15,-10.0055609537896));
#32002=CARTESIAN_POINT('Ctrl Pts',(-5.8611219075793,-0.0749999999999999,
-14.15));
#32003=CARTESIAN_POINT('Ctrl Pts',(0.,0.,-14.15));
#32004=CARTESIAN_POINT('Ctrl Pts',(5.86112190757929,0.0749999999999999,
-14.15));
#32005=CARTESIAN_POINT('Ctrl Pts',(10.0055609537896,0.15,-10.0055609537896));
#32006=CARTESIAN_POINT('Ctrl Pts',(14.15,0.225,-5.8611219075793));
#32007=CARTESIAN_POINT('Ctrl Pts',(14.15,0.299999999999999,-8.66437610396752E-16));
#32008=CARTESIAN_POINT('Ctrl Pts',(14.15,0.374999999999999,5.8611219075793));
#32009=CARTESIAN_POINT('Ctrl Pts',(10.0055609537896,0.449999999999999,10.0055609537896));
#32010=CARTESIAN_POINT('Ctrl Pts',(5.8611219075793,0.524999999999999,14.15));
#32011=CARTESIAN_POINT('Ctrl Pts',(1.7328752207935E-15,0.599999999999999,
14.15));
#32012=CARTESIAN_POINT('Ctrl Pts',(1.7328752207935E-15,0.599999999999999,
14.15));
#32013=CARTESIAN_POINT('Ctrl Pts',(-5.86112190757929,0.674999999999999,
14.15));
#32014=CARTESIAN_POINT('Ctrl Pts',(-10.0055609537896,0.749999999999998,
10.0055609537896));
#32015=CARTESIAN_POINT('Ctrl Pts',(-14.15,0.824999999999999,5.8611219075793));
#32016=CARTESIAN_POINT('Ctrl Pts',(-14.15,0.899999999999998,2.59931283119026E-15));
#32017=CARTESIAN_POINT('Ctrl Pts',(-14.15,0.974999999999998,-5.86112190757929));
#32018=CARTESIAN_POINT('Ctrl Pts',(-10.0055609537896,1.05,-10.0055609537896));
#32019=CARTESIAN_POINT('Ctrl Pts',(-5.8611219075793,1.125,-14.15));
#32020=CARTESIAN_POINT('Ctrl Pts',(-3.46575044158701E-15,1.2,-14.15));
#32021=CARTESIAN_POINT('Ctrl Pts',(5.86112190757929,1.275,-14.15));
#32022=CARTESIAN_POINT('Ctrl Pts',(10.0055609537896,1.35,-10.0055609537897));
#32023=CARTESIAN_POINT('Ctrl Pts',(14.15,1.425,-5.8611219075793));
#32024=CARTESIAN_POINT('Ctrl Pts',(14.15,1.5,-4.33218805198376E-15));
#32025=CARTESIAN_POINT('Ctrl Pts',(14.15,1.575,5.8611219075793));
#32026=CARTESIAN_POINT('Ctrl Pts',(10.0055609537897,1.65,10.0055609537896));
#32027=CARTESIAN_POINT('Ctrl Pts',(5.86112190757931,1.725,14.15));
#32028=CARTESIAN_POINT('Ctrl Pts',(5.19862566238051E-15,1.8,14.15));
#32029=CARTESIAN_POINT('Ctrl Pts',(-5.8611219075793,1.875,14.15));
#32030=CARTESIAN_POINT('Ctrl Pts',(-10.0055609537896,1.95,10.0055609537897));
#32031=CARTESIAN_POINT('Ctrl Pts',(-14.15,2.025,5.86112190757931));
#32032=CARTESIAN_POINT('Ctrl Pts',(-14.15,2.1,6.06506327277727E-15));
#32033=CARTESIAN_POINT('Ctrl Pts',(-14.15,2.175,-5.8611219075793));
#32034=CARTESIAN_POINT('Ctrl Pts',(-10.0055609537897,2.25,-10.0055609537896));
#32035=CARTESIAN_POINT('Ctrl Pts',(-5.86112190757931,2.32499999999999,-14.15));
#32036=CARTESIAN_POINT('Ctrl Pts',(-6.93150088317402E-15,2.4,-14.15));
#32037=CARTESIAN_POINT('Ctrl Pts',(5.86112190757929,2.475,-14.15));
#32038=CARTESIAN_POINT('Ctrl Pts',(10.0055609537896,2.54999999999999,-10.0055609537896));
#32039=CARTESIAN_POINT('Ctrl Pts',(14.15,2.625,-5.86112190757931));
#32040=CARTESIAN_POINT('Ctrl Pts',(14.15,2.69999999999999,-7.79793849357077E-15));
#32041=CARTESIAN_POINT('Ctrl Pts',(14.15,2.77499999999999,5.86112190757929));
#32042=CARTESIAN_POINT('Ctrl Pts',(10.0055609537897,2.84999999999999,10.0055609537896));
#32043=CARTESIAN_POINT('Ctrl Pts',(5.86112190757931,2.92499999999999,14.15));
#32044=CARTESIAN_POINT('Ctrl Pts',(8.66437610396752E-15,2.99999999999999,
14.15));
#32045=CARTESIAN_POINT('Ctrl Pts',(-5.86112190757929,3.07499999999999,14.15));
#32046=CARTESIAN_POINT('Ctrl Pts',(-10.0055609537896,3.14999999999999,10.0055609537896));
#32047=CARTESIAN_POINT('Ctrl Pts',(-14.15,3.22499999999999,5.86112190757931));
#32048=CARTESIAN_POINT('Ctrl Pts',(-14.15,3.29999999999999,9.53081371436428E-15));
#32049=CARTESIAN_POINT('Ctrl Pts',(-14.15,3.37499999999999,-5.86112190757929));
#32050=CARTESIAN_POINT('Ctrl Pts',(-10.0055609537897,3.44999999999999,-10.0055609537896));
#32051=CARTESIAN_POINT('Ctrl Pts',(-5.86112190757931,3.52499999999999,-14.15));
#32052=CARTESIAN_POINT('Ctrl Pts',(-1.0397251324761E-14,3.59999999999999,
-14.15));
#32053=CARTESIAN_POINT('Ctrl Pts',(5.86112190757927,3.67499999999999,-14.15));
#32054=CARTESIAN_POINT('Ctrl Pts',(10.0055609537896,3.74999999999999,-10.0055609537896));
#32055=CARTESIAN_POINT('Ctrl Pts',(14.15,3.82499999999999,-5.86112190757931));
#32056=CARTESIAN_POINT('Ctrl Pts',(14.15,3.89999999999999,-3.63991382126713E-14));
#32057=CARTESIAN_POINT('Ctrl Pts',(14.15,3.97499999999999,5.86112190757929));
#32058=CARTESIAN_POINT('Ctrl Pts',(10.0055609537897,4.04999999999999,10.0055609537896));
#32059=CARTESIAN_POINT('Ctrl Pts',(5.86112190757929,4.12499999999999,14.15));
#32060=CARTESIAN_POINT('Ctrl Pts',(1.21301265455545E-14,4.19999999999999,
14.15));
#32061=CARTESIAN_POINT('Origin',(-7.90471375114085E-13,4.8,14.15));
#32062=CARTESIAN_POINT('Ctrl Pts',(0.,7.34788079488412E-17,14.75));
#32063=CARTESIAN_POINT('Ctrl Pts',(-6.10965004500315,0.0749999999999999,
14.75));
#32064=CARTESIAN_POINT('Ctrl Pts',(-10.4298250225016,0.15,10.4298250225016));
#32065=CARTESIAN_POINT('Ctrl Pts',(-14.75,0.225,6.10965004500315));
#32066=CARTESIAN_POINT('Ctrl Pts',(-14.75,0.299999999999999,9.03177014371173E-16));
#32067=CARTESIAN_POINT('Ctrl Pts',(-14.75,0.374999999999999,-6.10965004500315));
#32068=CARTESIAN_POINT('Ctrl Pts',(-10.4298250225016,0.449999999999999,
-10.4298250225016));
#32069=CARTESIAN_POINT('Ctrl Pts',(-6.10965004500315,0.524999999999999,
-14.75));
#32070=CARTESIAN_POINT('Ctrl Pts',(-1.80635402874235E-15,0.599999999999999,
-14.75));
#32071=CARTESIAN_POINT('Ctrl Pts',(6.10965004500315,0.674999999999999,-14.75));
#32072=CARTESIAN_POINT('Ctrl Pts',(10.4298250225016,0.749999999999998,-10.4298250225016));
#32073=CARTESIAN_POINT('Ctrl Pts',(14.75,0.824999999999999,-6.10965004500316));
#32074=CARTESIAN_POINT('Ctrl Pts',(14.75,0.899999999999998,-2.70953104311352E-15));
#32075=CARTESIAN_POINT('Ctrl Pts',(14.75,0.974999999999998,6.10965004500316));
#32076=CARTESIAN_POINT('Ctrl Pts',(10.4298250225016,1.05,10.4298250225016));
#32077=CARTESIAN_POINT('Ctrl Pts',(6.10965004500316,1.125,14.75));
#32078=CARTESIAN_POINT('Ctrl Pts',(0.,1.2,14.75));
#32079=CARTESIAN_POINT('Ctrl Pts',(-6.10965004500315,1.275,14.75));
#32080=CARTESIAN_POINT('Ctrl Pts',(-10.4298250225016,1.35,10.4298250225016));
#32081=CARTESIAN_POINT('Ctrl Pts',(-14.75,1.425,6.10965004500315));
#32082=CARTESIAN_POINT('Ctrl Pts',(-14.75,1.5,9.03177014371173E-16));
#32083=CARTESIAN_POINT('Ctrl Pts',(-14.75,1.575,-6.10965004500315));
#32084=CARTESIAN_POINT('Ctrl Pts',(-10.4298250225016,1.65,-10.4298250225016));
#32085=CARTESIAN_POINT('Ctrl Pts',(-6.10965004500315,1.725,-14.75));
#32086=CARTESIAN_POINT('Ctrl Pts',(-1.80635402874235E-15,1.8,-14.75));
#32087=CARTESIAN_POINT('Ctrl Pts',(6.10965004500315,1.875,-14.75));
#32088=CARTESIAN_POINT('Ctrl Pts',(10.4298250225016,1.95,-10.4298250225016));
#32089=CARTESIAN_POINT('Ctrl Pts',(14.75,2.025,-6.10965004500316));
#32090=CARTESIAN_POINT('Ctrl Pts',(14.75,2.1,-2.70953104311352E-15));
#32091=CARTESIAN_POINT('Ctrl Pts',(14.75,2.17499999999999,6.10965004500316));
#32092=CARTESIAN_POINT('Ctrl Pts',(10.4298250225016,2.25,10.4298250225016));
#32093=CARTESIAN_POINT('Ctrl Pts',(6.10965004500316,2.32499999999999,14.75));
#32094=CARTESIAN_POINT('Ctrl Pts',(0.,2.39999999999999,14.75));
#32095=CARTESIAN_POINT('Ctrl Pts',(-6.10965004500315,2.47499999999999,14.75));
#32096=CARTESIAN_POINT('Ctrl Pts',(-10.4298250225016,2.54999999999999,10.4298250225016));
#32097=CARTESIAN_POINT('Ctrl Pts',(-14.75,2.62499999999999,6.10965004500315));
#32098=CARTESIAN_POINT('Ctrl Pts',(-14.75,2.69999999999999,9.03177014371173E-16));
#32099=CARTESIAN_POINT('Ctrl Pts',(-14.75,2.77499999999999,-6.10965004500315));
#32100=CARTESIAN_POINT('Ctrl Pts',(-10.4298250225016,2.84999999999999,-10.4298250225016));
#32101=CARTESIAN_POINT('Ctrl Pts',(-6.10965004500315,2.92499999999999,-14.75));
#32102=CARTESIAN_POINT('Ctrl Pts',(-1.80635402874235E-15,2.99999999999999,
-14.75));
#32103=CARTESIAN_POINT('Ctrl Pts',(6.10965004500315,3.07499999999999,-14.75));
#32104=CARTESIAN_POINT('Ctrl Pts',(10.4298250225016,3.14999999999999,-10.4298250225016));
#32105=CARTESIAN_POINT('Ctrl Pts',(14.75,3.22499999999999,-6.10965004500316));
#32106=CARTESIAN_POINT('Ctrl Pts',(14.75,3.29999999999999,-2.70953104311352E-15));
#32107=CARTESIAN_POINT('Ctrl Pts',(14.75,3.37499999999999,6.10965004500316));
#32108=CARTESIAN_POINT('Ctrl Pts',(10.4298250225016,3.44999999999999,10.4298250225016));
#32109=CARTESIAN_POINT('Ctrl Pts',(6.10965004500316,3.52499999999999,14.75));
#32110=CARTESIAN_POINT('Ctrl Pts',(0.,3.59999999999999,14.75));
#32111=CARTESIAN_POINT('Ctrl Pts',(-6.10965004500315,3.67499999999999,14.75));
#32112=CARTESIAN_POINT('Ctrl Pts',(-10.4298250225016,3.74999999999999,10.4298250225016));
#32113=CARTESIAN_POINT('Ctrl Pts',(-14.75,3.82499999999999,6.10965004500315));
#32114=CARTESIAN_POINT('Ctrl Pts',(-14.75,3.89999999999999,9.03177014371173E-16));
#32115=CARTESIAN_POINT('Ctrl Pts',(-14.75,3.97499999999999,-6.10965004500315));
#32116=CARTESIAN_POINT('Ctrl Pts',(-10.4298250225016,4.04999999999999,-10.4298250225016));
#32117=CARTESIAN_POINT('Ctrl Pts',(-6.10965004500315,4.12499999999999,-14.75));
#32118=CARTESIAN_POINT('Ctrl Pts',(-1.80635402874235E-15,4.19999999999999,
-14.75));
#32119=CARTESIAN_POINT('Ctrl Pts',(6.10965004500315,4.27499999999999,-14.75));
#32120=CARTESIAN_POINT('Ctrl Pts',(10.4298250225016,4.34999999999999,-10.4298250225016));
#32121=CARTESIAN_POINT('Ctrl Pts',(14.75,4.42499999999999,-6.10965004500316));
#32122=CARTESIAN_POINT('Ctrl Pts',(14.75,4.49999999999999,-2.70953104311352E-15));
#32123=CARTESIAN_POINT('Ctrl Pts',(14.75,4.57499999999999,6.10965004500316));
#32124=CARTESIAN_POINT('Ctrl Pts',(10.4298250225016,4.64999999999999,10.4298250225016));
#32125=CARTESIAN_POINT('Ctrl Pts',(6.10965004500316,4.72499999999999,14.75));
#32126=CARTESIAN_POINT('Ctrl Pts',(0.,4.79999999999999,14.75));
#32127=CARTESIAN_POINT('Ctrl Pts',(0.,-0.351471862576143,14.75));
#32128=CARTESIAN_POINT('Ctrl Pts',(-6.10965004500315,-0.276471862576143,
14.75));
#32129=CARTESIAN_POINT('Ctrl Pts',(-10.4298250225016,-0.201471862576143,
10.4298250225016));
#32130=CARTESIAN_POINT('Ctrl Pts',(-14.75,-0.126471862576144,6.10965004500315));
#32131=CARTESIAN_POINT('Ctrl Pts',(-14.75,-0.0514718625761437,9.03177014371173E-16));
#32132=CARTESIAN_POINT('Ctrl Pts',(-14.75,0.0235281374238561,-6.10965004500315));
#32133=CARTESIAN_POINT('Ctrl Pts',(-10.4298250225016,0.098528137423856,
-10.4298250225016));
#32134=CARTESIAN_POINT('Ctrl Pts',(-6.10965004500315,0.173528137423856,
-14.75));
#32135=CARTESIAN_POINT('Ctrl Pts',(-1.80635402874235E-15,0.248528137423856,
-14.75));
#32136=CARTESIAN_POINT('Ctrl Pts',(6.10965004500315,0.323528137423855,-14.75));
#32137=CARTESIAN_POINT('Ctrl Pts',(10.4298250225016,0.398528137423855,-10.4298250225016));
#32138=CARTESIAN_POINT('Ctrl Pts',(14.75,0.473528137423855,-6.10965004500316));
#32139=CARTESIAN_POINT('Ctrl Pts',(14.75,0.548528137423855,-2.70953104311352E-15));
#32140=CARTESIAN_POINT('Ctrl Pts',(14.75,0.623528137423855,6.10965004500316));
#32141=CARTESIAN_POINT('Ctrl Pts',(10.4298250225016,0.698528137423855,10.4298250225016));
#32142=CARTESIAN_POINT('Ctrl Pts',(6.10965004500316,0.773528137423855,14.75));
#32143=CARTESIAN_POINT('Ctrl Pts',(0.,0.848528137423854,14.75));
#32144=CARTESIAN_POINT('Ctrl Pts',(-6.10965004500315,0.923528137423854,
14.75));
#32145=CARTESIAN_POINT('Ctrl Pts',(-10.4298250225016,0.998528137423854,
10.4298250225016));
#32146=CARTESIAN_POINT('Ctrl Pts',(-14.75,1.07352813742385,6.10965004500315));
#32147=CARTESIAN_POINT('Ctrl Pts',(-14.75,1.14852813742385,9.03177014371173E-16));
#32148=CARTESIAN_POINT('Ctrl Pts',(-14.75,1.22352813742385,-6.10965004500315));
#32149=CARTESIAN_POINT('Ctrl Pts',(-10.4298250225016,1.29852813742385,-10.4298250225016));
#32150=CARTESIAN_POINT('Ctrl Pts',(-6.10965004500315,1.37352813742385,-14.75));
#32151=CARTESIAN_POINT('Ctrl Pts',(-1.80635402874235E-15,1.44852813742385,
-14.75));
#32152=CARTESIAN_POINT('Ctrl Pts',(6.10965004500315,1.52352813742385,-14.75));
#32153=CARTESIAN_POINT('Ctrl Pts',(10.4298250225016,1.59852813742385,-10.4298250225016));
#32154=CARTESIAN_POINT('Ctrl Pts',(14.75,1.67352813742385,-6.10965004500316));
#32155=CARTESIAN_POINT('Ctrl Pts',(14.75,1.74852813742385,-2.70953104311352E-15));
#32156=CARTESIAN_POINT('Ctrl Pts',(14.75,1.82352813742385,6.10965004500316));
#32157=CARTESIAN_POINT('Ctrl Pts',(10.4298250225016,1.89852813742385,10.4298250225016));
#32158=CARTESIAN_POINT('Ctrl Pts',(6.10965004500316,1.97352813742385,14.75));
#32159=CARTESIAN_POINT('Ctrl Pts',(0.,2.04852813742385,14.75));
#32160=CARTESIAN_POINT('Ctrl Pts',(-6.10965004500315,2.12352813742385,14.75));
#32161=CARTESIAN_POINT('Ctrl Pts',(-10.4298250225016,2.19852813742385,10.4298250225016));
#32162=CARTESIAN_POINT('Ctrl Pts',(-14.75,2.27352813742385,6.10965004500315));
#32163=CARTESIAN_POINT('Ctrl Pts',(-14.75,2.34852813742385,9.03177014371173E-16));
#32164=CARTESIAN_POINT('Ctrl Pts',(-14.75,2.42352813742385,-6.10965004500315));
#32165=CARTESIAN_POINT('Ctrl Pts',(-10.4298250225016,2.49852813742385,-10.4298250225016));
#32166=CARTESIAN_POINT('Ctrl Pts',(-6.10965004500315,2.57352813742385,-14.75));
#32167=CARTESIAN_POINT('Ctrl Pts',(-1.80635402874235E-15,2.64852813742385,
-14.75));
#32168=CARTESIAN_POINT('Ctrl Pts',(6.10965004500315,2.72352813742385,-14.75));
#32169=CARTESIAN_POINT('Ctrl Pts',(10.4298250225016,2.79852813742385,-10.4298250225016));
#32170=CARTESIAN_POINT('Ctrl Pts',(14.75,2.87352813742385,-6.10965004500316));
#32171=CARTESIAN_POINT('Ctrl Pts',(14.75,2.94852813742385,-2.70953104311352E-15));
#32172=CARTESIAN_POINT('Ctrl Pts',(14.75,3.02352813742385,6.10965004500316));
#32173=CARTESIAN_POINT('Ctrl Pts',(10.4298250225016,3.09852813742385,10.4298250225016));
#32174=CARTESIAN_POINT('Ctrl Pts',(6.10965004500316,3.17352813742385,14.75));
#32175=CARTESIAN_POINT('Ctrl Pts',(0.,3.24852813742385,14.75));
#32176=CARTESIAN_POINT('Ctrl Pts',(-6.10965004500315,3.32352813742385,14.75));
#32177=CARTESIAN_POINT('Ctrl Pts',(-10.4298250225016,3.39852813742385,10.4298250225016));
#32178=CARTESIAN_POINT('Ctrl Pts',(-14.75,3.47352813742385,6.10965004500315));
#32179=CARTESIAN_POINT('Ctrl Pts',(-14.75,3.54852813742385,9.03177014371173E-16));
#32180=CARTESIAN_POINT('Ctrl Pts',(-14.75,3.62352813742385,-6.10965004500315));
#32181=CARTESIAN_POINT('Ctrl Pts',(-10.4298250225016,3.69852813742385,-10.4298250225016));
#32182=CARTESIAN_POINT('Ctrl Pts',(-6.10965004500315,3.77352813742385,-14.75));
#32183=CARTESIAN_POINT('Ctrl Pts',(-1.80635402874235E-15,3.84852813742385,
-14.75));
#32184=CARTESIAN_POINT('Ctrl Pts',(6.10965004500315,3.92352813742385,-14.75));
#32185=CARTESIAN_POINT('Ctrl Pts',(10.4298250225016,3.99852813742385,-10.4298250225016));
#32186=CARTESIAN_POINT('Ctrl Pts',(14.75,4.07352813742385,-6.10965004500316));
#32187=CARTESIAN_POINT('Ctrl Pts',(14.75,4.14852813742385,-2.70953104311352E-15));
#32188=CARTESIAN_POINT('Ctrl Pts',(14.75,4.22352813742385,6.10965004500316));
#32189=CARTESIAN_POINT('Ctrl Pts',(10.4298250225016,4.29852813742385,10.4298250225016));
#32190=CARTESIAN_POINT('Ctrl Pts',(6.10965004500316,4.37352813742385,14.75));
#32191=CARTESIAN_POINT('Ctrl Pts',(0.,4.44852813742385,14.75));
#32192=CARTESIAN_POINT('Ctrl Pts',(0.,-0.6,14.5014718625761));
#32193=CARTESIAN_POINT('Ctrl Pts',(-6.00670631985087,-0.525,14.5014718625761));
#32194=CARTESIAN_POINT('Ctrl Pts',(-10.2540890912135,-0.45,10.2540890912135));
#32195=CARTESIAN_POINT('Ctrl Pts',(-14.5014718625761,-0.375000000000001,
6.00670631985087));
#32196=CARTESIAN_POINT('Ctrl Pts',(-14.5014718625761,-0.300000000000001,
8.87959054971464E-16));
#32197=CARTESIAN_POINT('Ctrl Pts',(-14.5014718625761,-0.225000000000001,
-6.00670631985087));
#32198=CARTESIAN_POINT('Ctrl Pts',(-10.2540890912135,-0.150000000000001,
-10.2540890912135));
#32199=CARTESIAN_POINT('Ctrl Pts',(-6.00670631985087,-0.0750000000000013,
-14.5014718625761));
#32200=CARTESIAN_POINT('Ctrl Pts',(-1.77591810994293E-15,-1.40946282423116E-15,
-14.5014718625761));
#32201=CARTESIAN_POINT('Ctrl Pts',(6.00670631985087,0.0749999999999985,
-14.5014718625761));
#32202=CARTESIAN_POINT('Ctrl Pts',(10.2540890912135,0.149999999999998,-10.2540890912135));
#32203=CARTESIAN_POINT('Ctrl Pts',(14.5014718625761,0.224999999999998,-6.00670631985087));
#32204=CARTESIAN_POINT('Ctrl Pts',(14.5014718625761,0.299999999999998,-2.66387716491439E-15));
#32205=CARTESIAN_POINT('Ctrl Pts',(14.5014718625761,0.374999999999998,6.00670631985087));
#32206=CARTESIAN_POINT('Ctrl Pts',(10.2540890912135,0.449999999999998,10.2540890912135));
#32207=CARTESIAN_POINT('Ctrl Pts',(6.00670631985088,0.524999999999997,14.5014718625761));
#32208=CARTESIAN_POINT('Ctrl Pts',(0.,0.599999999999997,14.5014718625761));
#32209=CARTESIAN_POINT('Ctrl Pts',(-6.00670631985087,0.674999999999997,
14.5014718625761));
#32210=CARTESIAN_POINT('Ctrl Pts',(-10.2540890912135,0.749999999999997,
10.2540890912135));
#32211=CARTESIAN_POINT('Ctrl Pts',(-14.5014718625761,0.824999999999997,
6.00670631985087));
#32212=CARTESIAN_POINT('Ctrl Pts',(-14.5014718625761,0.899999999999996,
8.87959054971464E-16));
#32213=CARTESIAN_POINT('Ctrl Pts',(-14.5014718625761,0.974999999999997,
-6.00670631985087));
#32214=CARTESIAN_POINT('Ctrl Pts',(-10.2540890912135,1.05,-10.2540890912135));
#32215=CARTESIAN_POINT('Ctrl Pts',(-6.00670631985087,1.125,-14.5014718625761));
#32216=CARTESIAN_POINT('Ctrl Pts',(-1.77591810994293E-15,1.2,-14.5014718625761));
#32217=CARTESIAN_POINT('Ctrl Pts',(6.00670631985087,1.275,-14.5014718625761));
#32218=CARTESIAN_POINT('Ctrl Pts',(10.2540890912135,1.35,-10.2540890912135));
#32219=CARTESIAN_POINT('Ctrl Pts',(14.5014718625761,1.425,-6.00670631985087));
#32220=CARTESIAN_POINT('Ctrl Pts',(14.5014718625761,1.5,-2.66387716491439E-15));
#32221=CARTESIAN_POINT('Ctrl Pts',(14.5014718625761,1.575,6.00670631985087));
#32222=CARTESIAN_POINT('Ctrl Pts',(10.2540890912135,1.65,10.2540890912135));
#32223=CARTESIAN_POINT('Ctrl Pts',(6.00670631985088,1.72499999999999,14.5014718625761));
#32224=CARTESIAN_POINT('Ctrl Pts',(0.,1.79999999999999,14.5014718625761));
#32225=CARTESIAN_POINT('Ctrl Pts',(-6.00670631985087,1.87499999999999,14.5014718625761));
#32226=CARTESIAN_POINT('Ctrl Pts',(-10.2540890912135,1.94999999999999,10.2540890912135));
#32227=CARTESIAN_POINT('Ctrl Pts',(-14.5014718625761,2.02499999999999,6.00670631985087));
#32228=CARTESIAN_POINT('Ctrl Pts',(-14.5014718625761,2.09999999999999,8.87959054971464E-16));
#32229=CARTESIAN_POINT('Ctrl Pts',(-14.5014718625761,2.17499999999999,-6.00670631985087));
#32230=CARTESIAN_POINT('Ctrl Pts',(-10.2540890912135,2.24999999999999,-10.2540890912135));
#32231=CARTESIAN_POINT('Ctrl Pts',(-6.00670631985087,2.32499999999999,-14.5014718625761));
#32232=CARTESIAN_POINT('Ctrl Pts',(-1.77591810994293E-15,2.39999999999999,
-14.5014718625761));
#32233=CARTESIAN_POINT('Ctrl Pts',(6.00670631985087,2.47499999999999,-14.5014718625761));
#32234=CARTESIAN_POINT('Ctrl Pts',(10.2540890912135,2.54999999999999,-10.2540890912135));
#32235=CARTESIAN_POINT('Ctrl Pts',(14.5014718625761,2.62499999999999,-6.00670631985087));
#32236=CARTESIAN_POINT('Ctrl Pts',(14.5014718625761,2.69999999999999,-2.66387716491439E-15));
#32237=CARTESIAN_POINT('Ctrl Pts',(14.5014718625761,2.77499999999999,6.00670631985087));
#32238=CARTESIAN_POINT('Ctrl Pts',(10.2540890912135,2.84999999999999,10.2540890912135));
#32239=CARTESIAN_POINT('Ctrl Pts',(6.00670631985088,2.92499999999999,14.5014718625761));
#32240=CARTESIAN_POINT('Ctrl Pts',(0.,2.99999999999999,14.5014718625761));
#32241=CARTESIAN_POINT('Ctrl Pts',(-6.00670631985087,3.07499999999999,14.5014718625761));
#32242=CARTESIAN_POINT('Ctrl Pts',(-10.2540890912135,3.14999999999999,10.2540890912135));
#32243=CARTESIAN_POINT('Ctrl Pts',(-14.5014718625761,3.22499999999999,6.00670631985087));
#32244=CARTESIAN_POINT('Ctrl Pts',(-14.5014718625761,3.29999999999999,8.87959054971464E-16));
#32245=CARTESIAN_POINT('Ctrl Pts',(-14.5014718625761,3.37499999999999,-6.00670631985087));
#32246=CARTESIAN_POINT('Ctrl Pts',(-10.2540890912135,3.44999999999999,-10.2540890912135));
#32247=CARTESIAN_POINT('Ctrl Pts',(-6.00670631985087,3.52499999999999,-14.5014718625761));
#32248=CARTESIAN_POINT('Ctrl Pts',(-1.77591810994293E-15,3.59999999999999,
-14.5014718625761));
#32249=CARTESIAN_POINT('Ctrl Pts',(6.00670631985087,3.67499999999999,-14.5014718625761));
#32250=CARTESIAN_POINT('Ctrl Pts',(10.2540890912135,3.74999999999999,-10.2540890912135));
#32251=CARTESIAN_POINT('Ctrl Pts',(14.5014718625761,3.82499999999999,-6.00670631985087));
#32252=CARTESIAN_POINT('Ctrl Pts',(14.5014718625761,3.89999999999999,-2.66387716491439E-15));
#32253=CARTESIAN_POINT('Ctrl Pts',(14.5014718625761,3.97499999999999,6.00670631985087));
#32254=CARTESIAN_POINT('Ctrl Pts',(10.2540890912135,4.04999999999999,10.2540890912135));
#32255=CARTESIAN_POINT('Ctrl Pts',(6.00670631985088,4.12499999999999,14.5014718625761));
#32256=CARTESIAN_POINT('Ctrl Pts',(0.,4.19999999999999,14.5014718625761));
#32257=CARTESIAN_POINT('Ctrl Pts',(0.,-0.6,14.15));
#32258=CARTESIAN_POINT('Ctrl Pts',(-5.8611219075793,-0.525,14.15));
#32259=CARTESIAN_POINT('Ctrl Pts',(-10.0055609537896,-0.450000000000001,
10.0055609537896));
#32260=CARTESIAN_POINT('Ctrl Pts',(-14.15,-0.375000000000001,5.8611219075793));
#32261=CARTESIAN_POINT('Ctrl Pts',(-14.15,-0.300000000000001,8.66437610396752E-16));
#32262=CARTESIAN_POINT('Ctrl Pts',(-14.15,-0.225000000000001,-5.86112190757929));
#32263=CARTESIAN_POINT('Ctrl Pts',(-10.0055609537896,-0.150000000000001,
-10.0055609537896));
#32264=CARTESIAN_POINT('Ctrl Pts',(-5.8611219075793,-0.0750000000000014,
-14.15));
#32265=CARTESIAN_POINT('Ctrl Pts',(-1.7328752207935E-15,-1.51788304147971E-15,
-14.15));
#32266=CARTESIAN_POINT('Ctrl Pts',(5.86112190757929,0.0749999999999984,
-14.15));
#32267=CARTESIAN_POINT('Ctrl Pts',(10.0055609537896,0.149999999999998,-10.0055609537896));
#32268=CARTESIAN_POINT('Ctrl Pts',(14.15,0.224999999999998,-5.8611219075793));
#32269=CARTESIAN_POINT('Ctrl Pts',(14.15,0.299999999999998,-2.59931283119026E-15));
#32270=CARTESIAN_POINT('Ctrl Pts',(14.15,0.374999999999998,5.8611219075793));
#32271=CARTESIAN_POINT('Ctrl Pts',(10.0055609537896,0.449999999999997,10.0055609537896));
#32272=CARTESIAN_POINT('Ctrl Pts',(5.8611219075793,0.524999999999997,14.15));
#32273=CARTESIAN_POINT('Ctrl Pts',(0.,0.599999999999997,14.15));
#32274=CARTESIAN_POINT('Ctrl Pts',(-5.8611219075793,0.674999999999997,14.15));
#32275=CARTESIAN_POINT('Ctrl Pts',(-10.0055609537896,0.749999999999997,
10.0055609537896));
#32276=CARTESIAN_POINT('Ctrl Pts',(-14.15,0.824999999999997,5.8611219075793));
#32277=CARTESIAN_POINT('Ctrl Pts',(-14.15,0.899999999999996,8.66437610396752E-16));
#32278=CARTESIAN_POINT('Ctrl Pts',(-14.15,0.974999999999996,-5.86112190757929));
#32279=CARTESIAN_POINT('Ctrl Pts',(-10.0055609537896,1.05,-10.0055609537896));
#32280=CARTESIAN_POINT('Ctrl Pts',(-5.8611219075793,1.125,-14.15));
#32281=CARTESIAN_POINT('Ctrl Pts',(-1.7328752207935E-15,1.2,-14.15));
#32282=CARTESIAN_POINT('Ctrl Pts',(5.86112190757929,1.275,-14.15));
#32283=CARTESIAN_POINT('Ctrl Pts',(10.0055609537896,1.35,-10.0055609537896));
#32284=CARTESIAN_POINT('Ctrl Pts',(14.15,1.425,-5.8611219075793));
#32285=CARTESIAN_POINT('Ctrl Pts',(14.15,1.49999999999999,-2.59931283119026E-15));
#32286=CARTESIAN_POINT('Ctrl Pts',(14.15,1.57499999999999,5.8611219075793));
#32287=CARTESIAN_POINT('Ctrl Pts',(10.0055609537896,1.64999999999999,10.0055609537896));
#32288=CARTESIAN_POINT('Ctrl Pts',(5.8611219075793,1.72499999999999,14.15));
#32289=CARTESIAN_POINT('Ctrl Pts',(0.,1.79999999999999,14.15));
#32290=CARTESIAN_POINT('Ctrl Pts',(-5.8611219075793,1.87499999999999,14.15));
#32291=CARTESIAN_POINT('Ctrl Pts',(-10.0055609537896,1.94999999999999,10.0055609537896));
#32292=CARTESIAN_POINT('Ctrl Pts',(-14.15,2.02499999999999,5.8611219075793));
#32293=CARTESIAN_POINT('Ctrl Pts',(-14.15,2.09999999999999,8.66437610396752E-16));
#32294=CARTESIAN_POINT('Ctrl Pts',(-14.15,2.17499999999999,-5.86112190757929));
#32295=CARTESIAN_POINT('Ctrl Pts',(-10.0055609537896,2.24999999999999,-10.0055609537896));
#32296=CARTESIAN_POINT('Ctrl Pts',(-5.8611219075793,2.32499999999999,-14.15));
#32297=CARTESIAN_POINT('Ctrl Pts',(-1.7328752207935E-15,2.39999999999999,
-14.15));
#32298=CARTESIAN_POINT('Ctrl Pts',(5.86112190757929,2.47499999999999,-14.15));
#32299=CARTESIAN_POINT('Ctrl Pts',(10.0055609537896,2.54999999999999,-10.0055609537896));
#32300=CARTESIAN_POINT('Ctrl Pts',(14.15,2.62499999999999,-5.8611219075793));
#32301=CARTESIAN_POINT('Ctrl Pts',(14.15,2.69999999999999,-2.59931283119026E-15));
#32302=CARTESIAN_POINT('Ctrl Pts',(14.15,2.77499999999999,5.8611219075793));
#32303=CARTESIAN_POINT('Ctrl Pts',(10.0055609537896,2.84999999999999,10.0055609537896));
#32304=CARTESIAN_POINT('Ctrl Pts',(5.8611219075793,2.92499999999999,14.15));
#32305=CARTESIAN_POINT('Ctrl Pts',(0.,2.99999999999999,14.15));
#32306=CARTESIAN_POINT('Ctrl Pts',(-5.8611219075793,3.07499999999999,14.15));
#32307=CARTESIAN_POINT('Ctrl Pts',(-10.0055609537896,3.14999999999999,10.0055609537896));
#32308=CARTESIAN_POINT('Ctrl Pts',(-14.15,3.22499999999999,5.8611219075793));
#32309=CARTESIAN_POINT('Ctrl Pts',(-14.15,3.29999999999999,8.66437610396752E-16));
#32310=CARTESIAN_POINT('Ctrl Pts',(-14.15,3.37499999999999,-5.86112190757929));
#32311=CARTESIAN_POINT('Ctrl Pts',(-10.0055609537896,3.44999999999999,-10.0055609537896));
#32312=CARTESIAN_POINT('Ctrl Pts',(-5.8611219075793,3.52499999999999,-14.15));
#32313=CARTESIAN_POINT('Ctrl Pts',(-1.7328752207935E-15,3.59999999999999,
-14.15));
#32314=CARTESIAN_POINT('Ctrl Pts',(5.86112190757929,3.67499999999999,-14.15));
#32315=CARTESIAN_POINT('Ctrl Pts',(10.0055609537896,3.74999999999999,-10.0055609537896));
#32316=CARTESIAN_POINT('Ctrl Pts',(14.15,3.82499999999999,-5.8611219075793));
#32317=CARTESIAN_POINT('Ctrl Pts',(14.15,3.89999999999999,-2.59931283119026E-15));
#32318=CARTESIAN_POINT('Ctrl Pts',(14.15,3.97499999999999,5.8611219075793));
#32319=CARTESIAN_POINT('Ctrl Pts',(10.0055609537896,4.04999999999999,10.0055609537896));
#32320=CARTESIAN_POINT('Ctrl Pts',(5.8611219075793,4.12499999999999,14.15));
#32321=CARTESIAN_POINT('Ctrl Pts',(0.,4.19999999999999,14.15));
#32322=CARTESIAN_POINT('',(0.,7.34788079488412E-17,14.75));
#32323=CARTESIAN_POINT('Origin',(0.,0.,14.15));
#32324=CARTESIAN_POINT('',(-4.0476938186852E-13,4.79999999999999,14.75));
#32325=CARTESIAN_POINT('Ctrl Pts',(0.,7.34788079488412E-17,14.75));
#32326=CARTESIAN_POINT('Ctrl Pts',(-6.10965004500315,0.0749999999999999,
14.75));
#32327=CARTESIAN_POINT('Ctrl Pts',(-10.4298250225016,0.15,10.4298250225016));
#32328=CARTESIAN_POINT('Ctrl Pts',(-14.75,0.225,6.10965004500315));
#32329=CARTESIAN_POINT('Ctrl Pts',(-14.75,0.299999999999999,9.03177014371173E-16));
#32330=CARTESIAN_POINT('Ctrl Pts',(-14.75,0.374999999999999,-6.10965004500315));
#32331=CARTESIAN_POINT('Ctrl Pts',(-10.4298250225016,0.449999999999999,
-10.4298250225016));
#32332=CARTESIAN_POINT('Ctrl Pts',(-6.10965004500315,0.524999999999999,
-14.75));
#32333=CARTESIAN_POINT('Ctrl Pts',(-1.80635402874235E-15,0.599999999999999,
-14.75));
#32334=CARTESIAN_POINT('Ctrl Pts',(6.10965004500315,0.674999999999999,-14.75));
#32335=CARTESIAN_POINT('Ctrl Pts',(10.4298250225016,0.749999999999998,-10.4298250225016));
#32336=CARTESIAN_POINT('Ctrl Pts',(14.75,0.824999999999999,-6.10965004500316));
#32337=CARTESIAN_POINT('Ctrl Pts',(14.75,0.899999999999998,-2.70953104311352E-15));
#32338=CARTESIAN_POINT('Ctrl Pts',(14.75,0.974999999999998,6.10965004500316));
#32339=CARTESIAN_POINT('Ctrl Pts',(10.4298250225016,1.05,10.4298250225016));
#32340=CARTESIAN_POINT('Ctrl Pts',(6.10965004500316,1.125,14.75));
#32341=CARTESIAN_POINT('Ctrl Pts',(3.61270805748469E-15,1.2,14.75));
#32342=CARTESIAN_POINT('Ctrl Pts',(-6.10965004500315,1.275,14.75));
#32343=CARTESIAN_POINT('Ctrl Pts',(-10.4298250225016,1.35,10.4298250225016));
#32344=CARTESIAN_POINT('Ctrl Pts',(-14.75,1.425,6.10965004500316));
#32345=CARTESIAN_POINT('Ctrl Pts',(-14.75,1.5,4.51588507185587E-15));
#32346=CARTESIAN_POINT('Ctrl Pts',(-14.75,1.575,-6.10965004500315));
#32347=CARTESIAN_POINT('Ctrl Pts',(-10.4298250225016,1.65,-10.4298250225016));
#32348=CARTESIAN_POINT('Ctrl Pts',(-6.10965004500316,1.725,-14.75));
#32349=CARTESIAN_POINT('Ctrl Pts',(-5.41906208622704E-15,1.8,-14.75));
#32350=CARTESIAN_POINT('Ctrl Pts',(6.10965004500315,1.875,-14.75));
#32351=CARTESIAN_POINT('Ctrl Pts',(10.4298250225016,1.95,-10.4298250225016));
#32352=CARTESIAN_POINT('Ctrl Pts',(14.75,2.025,-6.10965004500317));
#32353=CARTESIAN_POINT('Ctrl Pts',(14.75,2.1,-6.32223910059821E-15));
#32354=CARTESIAN_POINT('Ctrl Pts',(14.75,2.17499999999999,6.10965004500315));
#32355=CARTESIAN_POINT('Ctrl Pts',(10.4298250225016,2.25,10.4298250225016));
#32356=CARTESIAN_POINT('Ctrl Pts',(6.10965004500317,2.32499999999999,14.75));
#32357=CARTESIAN_POINT('Ctrl Pts',(7.22541611496938E-15,2.39999999999999,
14.75));
#32358=CARTESIAN_POINT('Ctrl Pts',(-6.10965004500315,2.475,14.75));
#32359=CARTESIAN_POINT('Ctrl Pts',(-10.4298250225016,2.54999999999999,10.4298250225016));
#32360=CARTESIAN_POINT('Ctrl Pts',(-14.75,2.62499999999999,6.10965004500317));
#32361=CARTESIAN_POINT('Ctrl Pts',(-14.75,2.69999999999999,8.12859312934056E-15));
#32362=CARTESIAN_POINT('Ctrl Pts',(-14.75,2.77499999999999,-6.10965004500315));
#32363=CARTESIAN_POINT('Ctrl Pts',(-10.4298250225016,2.84999999999999,-10.4298250225016));
#32364=CARTESIAN_POINT('Ctrl Pts',(-6.10965004500317,2.92499999999999,-14.75));
#32365=CARTESIAN_POINT('Ctrl Pts',(-9.03177014371173E-15,2.99999999999999,
-14.75));
#32366=CARTESIAN_POINT('Ctrl Pts',(6.10965004500312,3.07499999999999,-14.75));
#32367=CARTESIAN_POINT('Ctrl Pts',(10.4298250225016,3.14999999999999,-10.4298250225016));
#32368=CARTESIAN_POINT('Ctrl Pts',(14.75,3.22499999999999,-6.10965004500317));
#32369=CARTESIAN_POINT('Ctrl Pts',(14.75,3.29999999999999,-3.61362105392366E-14));
#32370=CARTESIAN_POINT('Ctrl Pts',(14.75,3.37499999999999,6.10965004500315));
#32371=CARTESIAN_POINT('Ctrl Pts',(10.4298250225016,3.44999999999999,10.4298250225016));
#32372=CARTESIAN_POINT('Ctrl Pts',(6.10965004500314,3.52499999999999,14.75));
#32373=CARTESIAN_POINT('Ctrl Pts',(1.08381241724541E-14,3.59999999999999,
14.75));
#32374=CARTESIAN_POINT('Ctrl Pts',(-6.10965004500312,3.67499999999999,14.75));
#32375=CARTESIAN_POINT('Ctrl Pts',(-10.4298250225016,3.74999999999999,10.4298250225016));
#32376=CARTESIAN_POINT('Ctrl Pts',(-14.75,3.82499999999999,6.10965004500317));
#32377=CARTESIAN_POINT('Ctrl Pts',(-14.75,3.89999999999999,-1.44599621943284E-14));
#32378=CARTESIAN_POINT('Ctrl Pts',(-14.75,3.97499999999999,-6.10965004500315));
#32379=CARTESIAN_POINT('Ctrl Pts',(-10.4298250225016,4.04999999999999,-10.4298250225016));
#32380=CARTESIAN_POINT('Ctrl Pts',(-6.10965004500315,4.12499999999999,-14.75));
#32381=CARTESIAN_POINT('Ctrl Pts',(-1.26444782011964E-14,4.19999999999999,
-14.75));
#32382=CARTESIAN_POINT('Ctrl Pts',(6.10965004500312,4.27499999999999,-14.75));
#32383=CARTESIAN_POINT('Ctrl Pts',(10.4298250225016,4.34999999999999,-10.4298250225016));
#32384=CARTESIAN_POINT('Ctrl Pts',(14.75,4.42499999999999,-6.10965004500317));
#32385=CARTESIAN_POINT('Ctrl Pts',(14.75,4.49999999999999,-3.97489185967213E-14));
#32386=CARTESIAN_POINT('Ctrl Pts',(14.75,4.57499999999999,6.10965004500315));
#32387=CARTESIAN_POINT('Ctrl Pts',(10.4298250225016,4.64999999999999,10.4298250225016));
#32388=CARTESIAN_POINT('Ctrl Pts',(6.10965004500315,4.72499999999999,14.75));
#32389=CARTESIAN_POINT('Ctrl Pts',(-4.0476938186852E-13,4.79999999999999,
14.75));
#32390=CARTESIAN_POINT('Origin',(-7.90471375114085E-13,4.8,14.15));
#32391=CARTESIAN_POINT('Ctrl Pts',(0.,0.6,14.15));
#32392=CARTESIAN_POINT('Ctrl Pts',(-5.8611219075793,0.675,14.15));
#32393=CARTESIAN_POINT('Ctrl Pts',(-10.0055609537896,0.75,10.0055609537896));
#32394=CARTESIAN_POINT('Ctrl Pts',(-14.15,0.825,5.8611219075793));
#32395=CARTESIAN_POINT('Ctrl Pts',(-14.15,0.9,8.66437610396752E-16));
#32396=CARTESIAN_POINT('Ctrl Pts',(-14.15,0.974999999999999,-5.86112190757929));
#32397=CARTESIAN_POINT('Ctrl Pts',(-10.0055609537896,1.05,-10.0055609537896));
#32398=CARTESIAN_POINT('Ctrl Pts',(-5.8611219075793,1.125,-14.15));
#32399=CARTESIAN_POINT('Ctrl Pts',(-1.7328752207935E-15,1.2,-14.15));
#32400=CARTESIAN_POINT('Ctrl Pts',(5.86112190757929,1.275,-14.15));
#32401=CARTESIAN_POINT('Ctrl Pts',(10.0055609537896,1.35,-10.0055609537896));
#32402=CARTESIAN_POINT('Ctrl Pts',(14.15,1.425,-5.8611219075793));
#32403=CARTESIAN_POINT('Ctrl Pts',(14.15,1.5,-2.59931283119026E-15));
#32404=CARTESIAN_POINT('Ctrl Pts',(14.15,1.575,5.8611219075793));
#32405=CARTESIAN_POINT('Ctrl Pts',(10.0055609537896,1.65,10.0055609537896));
#32406=CARTESIAN_POINT('Ctrl Pts',(5.8611219075793,1.725,14.15));
#32407=CARTESIAN_POINT('Ctrl Pts',(0.,1.8,14.15));
#32408=CARTESIAN_POINT('Ctrl Pts',(-5.8611219075793,1.875,14.15));
#32409=CARTESIAN_POINT('Ctrl Pts',(-10.0055609537896,1.95,10.0055609537896));
#32410=CARTESIAN_POINT('Ctrl Pts',(-14.15,2.025,5.8611219075793));
#32411=CARTESIAN_POINT('Ctrl Pts',(-14.15,2.1,8.66437610396752E-16));
#32412=CARTESIAN_POINT('Ctrl Pts',(-14.15,2.175,-5.86112190757929));
#32413=CARTESIAN_POINT('Ctrl Pts',(-10.0055609537896,2.25,-10.0055609537896));
#32414=CARTESIAN_POINT('Ctrl Pts',(-5.8611219075793,2.325,-14.15));
#32415=CARTESIAN_POINT('Ctrl Pts',(-1.7328752207935E-15,2.4,-14.15));
#32416=CARTESIAN_POINT('Ctrl Pts',(5.86112190757929,2.475,-14.15));
#32417=CARTESIAN_POINT('Ctrl Pts',(10.0055609537896,2.55,-10.0055609537896));
#32418=CARTESIAN_POINT('Ctrl Pts',(14.15,2.625,-5.8611219075793));
#32419=CARTESIAN_POINT('Ctrl Pts',(14.15,2.7,-2.59931283119026E-15));
#32420=CARTESIAN_POINT('Ctrl Pts',(14.15,2.775,5.8611219075793));
#32421=CARTESIAN_POINT('Ctrl Pts',(10.0055609537896,2.85,10.0055609537896));
#32422=CARTESIAN_POINT('Ctrl Pts',(5.8611219075793,2.92499999999999,14.15));
#32423=CARTESIAN_POINT('Ctrl Pts',(0.,2.99999999999999,14.15));
#32424=CARTESIAN_POINT('Ctrl Pts',(-5.8611219075793,3.07499999999999,14.15));
#32425=CARTESIAN_POINT('Ctrl Pts',(-10.0055609537896,3.15,10.0055609537896));
#32426=CARTESIAN_POINT('Ctrl Pts',(-14.15,3.22499999999999,5.8611219075793));
#32427=CARTESIAN_POINT('Ctrl Pts',(-14.15,3.29999999999999,8.66437610396752E-16));
#32428=CARTESIAN_POINT('Ctrl Pts',(-14.15,3.37499999999999,-5.86112190757929));
#32429=CARTESIAN_POINT('Ctrl Pts',(-10.0055609537896,3.44999999999999,-10.0055609537896));
#32430=CARTESIAN_POINT('Ctrl Pts',(-5.8611219075793,3.52499999999999,-14.15));
#32431=CARTESIAN_POINT('Ctrl Pts',(-1.7328752207935E-15,3.59999999999999,
-14.15));
#32432=CARTESIAN_POINT('Ctrl Pts',(5.86112190757929,3.67499999999999,-14.15));
#32433=CARTESIAN_POINT('Ctrl Pts',(10.0055609537896,3.74999999999999,-10.0055609537896));
#32434=CARTESIAN_POINT('Ctrl Pts',(14.15,3.82499999999999,-5.8611219075793));
#32435=CARTESIAN_POINT('Ctrl Pts',(14.15,3.89999999999999,-2.59931283119026E-15));
#32436=CARTESIAN_POINT('Ctrl Pts',(14.15,3.97499999999999,5.8611219075793));
#32437=CARTESIAN_POINT('Ctrl Pts',(10.0055609537896,4.04999999999999,10.0055609537896));
#32438=CARTESIAN_POINT('Ctrl Pts',(5.8611219075793,4.12499999999999,14.15));
#32439=CARTESIAN_POINT('Ctrl Pts',(0.,4.19999999999999,14.15));
#32440=CARTESIAN_POINT('Ctrl Pts',(-5.8611219075793,4.27499999999999,14.15));
#32441=CARTESIAN_POINT('Ctrl Pts',(-10.0055609537896,4.34999999999999,10.0055609537896));
#32442=CARTESIAN_POINT('Ctrl Pts',(-14.15,4.42499999999999,5.8611219075793));
#32443=CARTESIAN_POINT('Ctrl Pts',(-14.15,4.49999999999999,8.66437610396752E-16));
#32444=CARTESIAN_POINT('Ctrl Pts',(-14.15,4.57499999999999,-5.86112190757929));
#32445=CARTESIAN_POINT('Ctrl Pts',(-10.0055609537896,4.64999999999999,-10.0055609537896));
#32446=CARTESIAN_POINT('Ctrl Pts',(-5.8611219075793,4.72499999999999,-14.15));
#32447=CARTESIAN_POINT('Ctrl Pts',(-1.7328752207935E-15,4.79999999999999,
-14.15));
#32448=CARTESIAN_POINT('Ctrl Pts',(5.86112190757929,4.87499999999999,-14.15));
#32449=CARTESIAN_POINT('Ctrl Pts',(10.0055609537896,4.94999999999999,-10.0055609537896));
#32450=CARTESIAN_POINT('Ctrl Pts',(14.15,5.02499999999999,-5.8611219075793));
#32451=CARTESIAN_POINT('Ctrl Pts',(14.15,5.09999999999999,-2.59931283119026E-15));
#32452=CARTESIAN_POINT('Ctrl Pts',(14.15,5.17499999999999,5.8611219075793));
#32453=CARTESIAN_POINT('Ctrl Pts',(10.0055609537896,5.24999999999999,10.0055609537896));
#32454=CARTESIAN_POINT('Ctrl Pts',(5.8611219075793,5.32499999999999,14.15));
#32455=CARTESIAN_POINT('Ctrl Pts',(0.,5.39999999999999,14.15));
#32456=CARTESIAN_POINT('Ctrl Pts',(0.,0.6,14.5014718625761));
#32457=CARTESIAN_POINT('Ctrl Pts',(-6.00670631985087,0.675,14.5014718625761));
#32458=CARTESIAN_POINT('Ctrl Pts',(-10.2540890912135,0.75,10.2540890912135));
#32459=CARTESIAN_POINT('Ctrl Pts',(-14.5014718625761,0.825,6.00670631985087));
#32460=CARTESIAN_POINT('Ctrl Pts',(-14.5014718625761,0.9,8.87959054971464E-16));
#32461=CARTESIAN_POINT('Ctrl Pts',(-14.5014718625761,0.974999999999999,
-6.00670631985087));
#32462=CARTESIAN_POINT('Ctrl Pts',(-10.2540890912135,1.05,-10.2540890912135));
#32463=CARTESIAN_POINT('Ctrl Pts',(-6.00670631985087,1.125,-14.5014718625761));
#32464=CARTESIAN_POINT('Ctrl Pts',(-1.77591810994293E-15,1.2,-14.5014718625761));
#32465=CARTESIAN_POINT('Ctrl Pts',(6.00670631985087,1.275,-14.5014718625761));
#32466=CARTESIAN_POINT('Ctrl Pts',(10.2540890912135,1.35,-10.2540890912135));
#32467=CARTESIAN_POINT('Ctrl Pts',(14.5014718625761,1.425,-6.00670631985087));
#32468=CARTESIAN_POINT('Ctrl Pts',(14.5014718625761,1.5,-2.66387716491439E-15));
#32469=CARTESIAN_POINT('Ctrl Pts',(14.5014718625761,1.575,6.00670631985087));
#32470=CARTESIAN_POINT('Ctrl Pts',(10.2540890912135,1.65,10.2540890912135));
#32471=CARTESIAN_POINT('Ctrl Pts',(6.00670631985088,1.725,14.5014718625761));
#32472=CARTESIAN_POINT('Ctrl Pts',(0.,1.8,14.5014718625761));
#32473=CARTESIAN_POINT('Ctrl Pts',(-6.00670631985087,1.875,14.5014718625761));
#32474=CARTESIAN_POINT('Ctrl Pts',(-10.2540890912135,1.95,10.2540890912135));
#32475=CARTESIAN_POINT('Ctrl Pts',(-14.5014718625761,2.025,6.00670631985087));
#32476=CARTESIAN_POINT('Ctrl Pts',(-14.5014718625761,2.1,8.87959054971464E-16));
#32477=CARTESIAN_POINT('Ctrl Pts',(-14.5014718625761,2.175,-6.00670631985087));
#32478=CARTESIAN_POINT('Ctrl Pts',(-10.2540890912135,2.25,-10.2540890912135));
#32479=CARTESIAN_POINT('Ctrl Pts',(-6.00670631985087,2.325,-14.5014718625761));
#32480=CARTESIAN_POINT('Ctrl Pts',(-1.77591810994293E-15,2.4,-14.5014718625761));
#32481=CARTESIAN_POINT('Ctrl Pts',(6.00670631985087,2.475,-14.5014718625761));
#32482=CARTESIAN_POINT('Ctrl Pts',(10.2540890912135,2.55,-10.2540890912135));
#32483=CARTESIAN_POINT('Ctrl Pts',(14.5014718625761,2.625,-6.00670631985087));
#32484=CARTESIAN_POINT('Ctrl Pts',(14.5014718625761,2.7,-2.66387716491439E-15));
#32485=CARTESIAN_POINT('Ctrl Pts',(14.5014718625761,2.775,6.00670631985087));
#32486=CARTESIAN_POINT('Ctrl Pts',(10.2540890912135,2.85,10.2540890912135));
#32487=CARTESIAN_POINT('Ctrl Pts',(6.00670631985088,2.92499999999999,14.5014718625761));
#32488=CARTESIAN_POINT('Ctrl Pts',(0.,2.99999999999999,14.5014718625761));
#32489=CARTESIAN_POINT('Ctrl Pts',(-6.00670631985087,3.075,14.5014718625761));
#32490=CARTESIAN_POINT('Ctrl Pts',(-10.2540890912135,3.14999999999999,10.2540890912135));
#32491=CARTESIAN_POINT('Ctrl Pts',(-14.5014718625761,3.22499999999999,6.00670631985087));
#32492=CARTESIAN_POINT('Ctrl Pts',(-14.5014718625761,3.29999999999999,8.87959054971464E-16));
#32493=CARTESIAN_POINT('Ctrl Pts',(-14.5014718625761,3.37499999999999,-6.00670631985087));
#32494=CARTESIAN_POINT('Ctrl Pts',(-10.2540890912135,3.44999999999999,-10.2540890912135));
#32495=CARTESIAN_POINT('Ctrl Pts',(-6.00670631985087,3.52499999999999,-14.5014718625761));
#32496=CARTESIAN_POINT('Ctrl Pts',(-1.77591810994293E-15,3.59999999999999,
-14.5014718625761));
#32497=CARTESIAN_POINT('Ctrl Pts',(6.00670631985087,3.67499999999999,-14.5014718625761));
#32498=CARTESIAN_POINT('Ctrl Pts',(10.2540890912135,3.74999999999999,-10.2540890912135));
#32499=CARTESIAN_POINT('Ctrl Pts',(14.5014718625761,3.82499999999999,-6.00670631985087));
#32500=CARTESIAN_POINT('Ctrl Pts',(14.5014718625761,3.89999999999999,-2.66387716491439E-15));
#32501=CARTESIAN_POINT('Ctrl Pts',(14.5014718625761,3.97499999999999,6.00670631985087));
#32502=CARTESIAN_POINT('Ctrl Pts',(10.2540890912135,4.04999999999999,10.2540890912135));
#32503=CARTESIAN_POINT('Ctrl Pts',(6.00670631985088,4.12499999999999,14.5014718625761));
#32504=CARTESIAN_POINT('Ctrl Pts',(0.,4.19999999999999,14.5014718625761));
#32505=CARTESIAN_POINT('Ctrl Pts',(-6.00670631985087,4.27499999999999,14.5014718625761));
#32506=CARTESIAN_POINT('Ctrl Pts',(-10.2540890912135,4.34999999999999,10.2540890912135));
#32507=CARTESIAN_POINT('Ctrl Pts',(-14.5014718625761,4.42499999999999,6.00670631985087));
#32508=CARTESIAN_POINT('Ctrl Pts',(-14.5014718625761,4.49999999999999,8.87959054971464E-16));
#32509=CARTESIAN_POINT('Ctrl Pts',(-14.5014718625761,4.57499999999999,-6.00670631985087));
#32510=CARTESIAN_POINT('Ctrl Pts',(-10.2540890912135,4.64999999999999,-10.2540890912135));
#32511=CARTESIAN_POINT('Ctrl Pts',(-6.00670631985087,4.72499999999999,-14.5014718625761));
#32512=CARTESIAN_POINT('Ctrl Pts',(-1.77591810994293E-15,4.79999999999999,
-14.5014718625761));
#32513=CARTESIAN_POINT('Ctrl Pts',(6.00670631985087,4.87499999999999,-14.5014718625761));
#32514=CARTESIAN_POINT('Ctrl Pts',(10.2540890912135,4.94999999999999,-10.2540890912135));
#32515=CARTESIAN_POINT('Ctrl Pts',(14.5014718625761,5.02499999999999,-6.00670631985087));
#32516=CARTESIAN_POINT('Ctrl Pts',(14.5014718625761,5.09999999999999,-2.66387716491439E-15));
#32517=CARTESIAN_POINT('Ctrl Pts',(14.5014718625761,5.17499999999999,6.00670631985087));
#32518=CARTESIAN_POINT('Ctrl Pts',(10.2540890912135,5.24999999999999,10.2540890912135));
#32519=CARTESIAN_POINT('Ctrl Pts',(6.00670631985088,5.32499999999999,14.5014718625761));
#32520=CARTESIAN_POINT('Ctrl Pts',(0.,5.39999999999999,14.5014718625761));
#32521=CARTESIAN_POINT('Ctrl Pts',(0.,0.351471862576143,14.75));
#32522=CARTESIAN_POINT('Ctrl Pts',(-6.10965004500315,0.426471862576143,
14.75));
#32523=CARTESIAN_POINT('Ctrl Pts',(-10.4298250225016,0.501471862576143,
10.4298250225016));
#32524=CARTESIAN_POINT('Ctrl Pts',(-14.75,0.576471862576143,6.10965004500315));
#32525=CARTESIAN_POINT('Ctrl Pts',(-14.75,0.651471862576142,9.03177014371173E-16));
#32526=CARTESIAN_POINT('Ctrl Pts',(-14.75,0.726471862576142,-6.10965004500315));
#32527=CARTESIAN_POINT('Ctrl Pts',(-10.4298250225016,0.801471862576142,
-10.4298250225016));
#32528=CARTESIAN_POINT('Ctrl Pts',(-6.10965004500315,0.876471862576142,
-14.75));
#32529=CARTESIAN_POINT('Ctrl Pts',(-1.80635402874235E-15,0.951471862576142,
-14.75));
#32530=CARTESIAN_POINT('Ctrl Pts',(6.10965004500315,1.02647186257614,-14.75));
#32531=CARTESIAN_POINT('Ctrl Pts',(10.4298250225016,1.10147186257614,-10.4298250225016));
#32532=CARTESIAN_POINT('Ctrl Pts',(14.75,1.17647186257614,-6.10965004500316));
#32533=CARTESIAN_POINT('Ctrl Pts',(14.75,1.25147186257614,-2.70953104311352E-15));
#32534=CARTESIAN_POINT('Ctrl Pts',(14.75,1.32647186257614,6.10965004500316));
#32535=CARTESIAN_POINT('Ctrl Pts',(10.4298250225016,1.40147186257614,10.4298250225016));
#32536=CARTESIAN_POINT('Ctrl Pts',(6.10965004500316,1.47647186257614,14.75));
#32537=CARTESIAN_POINT('Ctrl Pts',(0.,1.55147186257614,14.75));
#32538=CARTESIAN_POINT('Ctrl Pts',(-6.10965004500315,1.62647186257614,14.75));
#32539=CARTESIAN_POINT('Ctrl Pts',(-10.4298250225016,1.70147186257614,10.4298250225016));
#32540=CARTESIAN_POINT('Ctrl Pts',(-14.75,1.77647186257614,6.10965004500315));
#32541=CARTESIAN_POINT('Ctrl Pts',(-14.75,1.85147186257614,9.03177014371173E-16));
#32542=CARTESIAN_POINT('Ctrl Pts',(-14.75,1.92647186257614,-6.10965004500315));
#32543=CARTESIAN_POINT('Ctrl Pts',(-10.4298250225016,2.00147186257614,-10.4298250225016));
#32544=CARTESIAN_POINT('Ctrl Pts',(-6.10965004500315,2.07647186257614,-14.75));
#32545=CARTESIAN_POINT('Ctrl Pts',(-1.80635402874235E-15,2.15147186257614,
-14.75));
#32546=CARTESIAN_POINT('Ctrl Pts',(6.10965004500315,2.22647186257614,-14.75));
#32547=CARTESIAN_POINT('Ctrl Pts',(10.4298250225016,2.30147186257614,-10.4298250225016));
#32548=CARTESIAN_POINT('Ctrl Pts',(14.75,2.37647186257614,-6.10965004500316));
#32549=CARTESIAN_POINT('Ctrl Pts',(14.75,2.45147186257614,-2.70953104311352E-15));
#32550=CARTESIAN_POINT('Ctrl Pts',(14.75,2.52647186257614,6.10965004500316));
#32551=CARTESIAN_POINT('Ctrl Pts',(10.4298250225016,2.60147186257614,10.4298250225016));
#32552=CARTESIAN_POINT('Ctrl Pts',(6.10965004500316,2.67647186257614,14.75));
#32553=CARTESIAN_POINT('Ctrl Pts',(0.,2.75147186257614,14.75));
#32554=CARTESIAN_POINT('Ctrl Pts',(-6.10965004500315,2.82647186257614,14.75));
#32555=CARTESIAN_POINT('Ctrl Pts',(-10.4298250225016,2.90147186257614,10.4298250225016));
#32556=CARTESIAN_POINT('Ctrl Pts',(-14.75,2.97647186257614,6.10965004500315));
#32557=CARTESIAN_POINT('Ctrl Pts',(-14.75,3.05147186257614,9.03177014371173E-16));
#32558=CARTESIAN_POINT('Ctrl Pts',(-14.75,3.12647186257614,-6.10965004500315));
#32559=CARTESIAN_POINT('Ctrl Pts',(-10.4298250225016,3.20147186257614,-10.4298250225016));
#32560=CARTESIAN_POINT('Ctrl Pts',(-6.10965004500315,3.27647186257614,-14.75));
#32561=CARTESIAN_POINT('Ctrl Pts',(-1.80635402874235E-15,3.35147186257614,
-14.75));
#32562=CARTESIAN_POINT('Ctrl Pts',(6.10965004500315,3.42647186257614,-14.75));
#32563=CARTESIAN_POINT('Ctrl Pts',(10.4298250225016,3.50147186257614,-10.4298250225016));
#32564=CARTESIAN_POINT('Ctrl Pts',(14.75,3.57647186257614,-6.10965004500316));
#32565=CARTESIAN_POINT('Ctrl Pts',(14.75,3.65147186257614,-2.70953104311352E-15));
#32566=CARTESIAN_POINT('Ctrl Pts',(14.75,3.72647186257614,6.10965004500316));
#32567=CARTESIAN_POINT('Ctrl Pts',(10.4298250225016,3.80147186257614,10.4298250225016));
#32568=CARTESIAN_POINT('Ctrl Pts',(6.10965004500316,3.87647186257614,14.75));
#32569=CARTESIAN_POINT('Ctrl Pts',(0.,3.95147186257614,14.75));
#32570=CARTESIAN_POINT('Ctrl Pts',(-6.10965004500315,4.02647186257614,14.75));
#32571=CARTESIAN_POINT('Ctrl Pts',(-10.4298250225016,4.10147186257613,10.4298250225016));
#32572=CARTESIAN_POINT('Ctrl Pts',(-14.75,4.17647186257613,6.10965004500315));
#32573=CARTESIAN_POINT('Ctrl Pts',(-14.75,4.25147186257614,9.03177014371173E-16));
#32574=CARTESIAN_POINT('Ctrl Pts',(-14.75,4.32647186257613,-6.10965004500315));
#32575=CARTESIAN_POINT('Ctrl Pts',(-10.4298250225016,4.40147186257613,-10.4298250225016));
#32576=CARTESIAN_POINT('Ctrl Pts',(-6.10965004500315,4.47647186257614,-14.75));
#32577=CARTESIAN_POINT('Ctrl Pts',(-1.80635402874235E-15,4.55147186257613,
-14.75));
#32578=CARTESIAN_POINT('Ctrl Pts',(6.10965004500315,4.62647186257613,-14.75));
#32579=CARTESIAN_POINT('Ctrl Pts',(10.4298250225016,4.70147186257613,-10.4298250225016));
#32580=CARTESIAN_POINT('Ctrl Pts',(14.75,4.77647186257613,-6.10965004500316));
#32581=CARTESIAN_POINT('Ctrl Pts',(14.75,4.85147186257613,-2.70953104311352E-15));
#32582=CARTESIAN_POINT('Ctrl Pts',(14.75,4.92647186257613,6.10965004500316));
#32583=CARTESIAN_POINT('Ctrl Pts',(10.4298250225016,5.00147186257613,10.4298250225016));
#32584=CARTESIAN_POINT('Ctrl Pts',(6.10965004500316,5.07647186257613,14.75));
#32585=CARTESIAN_POINT('Ctrl Pts',(0.,5.15147186257613,14.75));
#32586=CARTESIAN_POINT('Ctrl Pts',(0.,7.34788079488412E-17,14.75));
#32587=CARTESIAN_POINT('Ctrl Pts',(-6.10965004500315,0.0749999999999999,
14.75));
#32588=CARTESIAN_POINT('Ctrl Pts',(-10.4298250225016,0.15,10.4298250225016));
#32589=CARTESIAN_POINT('Ctrl Pts',(-14.75,0.225,6.10965004500315));
#32590=CARTESIAN_POINT('Ctrl Pts',(-14.75,0.299999999999999,9.03177014371173E-16));
#32591=CARTESIAN_POINT('Ctrl Pts',(-14.75,0.374999999999999,-6.10965004500315));
#32592=CARTESIAN_POINT('Ctrl Pts',(-10.4298250225016,0.449999999999999,
-10.4298250225016));
#32593=CARTESIAN_POINT('Ctrl Pts',(-6.10965004500315,0.524999999999999,
-14.75));
#32594=CARTESIAN_POINT('Ctrl Pts',(-1.80635402874235E-15,0.599999999999999,
-14.75));
#32595=CARTESIAN_POINT('Ctrl Pts',(6.10965004500315,0.674999999999999,-14.75));
#32596=CARTESIAN_POINT('Ctrl Pts',(10.4298250225016,0.749999999999998,-10.4298250225016));
#32597=CARTESIAN_POINT('Ctrl Pts',(14.75,0.824999999999999,-6.10965004500316));
#32598=CARTESIAN_POINT('Ctrl Pts',(14.75,0.899999999999998,-2.70953104311352E-15));
#32599=CARTESIAN_POINT('Ctrl Pts',(14.75,0.974999999999998,6.10965004500316));
#32600=CARTESIAN_POINT('Ctrl Pts',(10.4298250225016,1.05,10.4298250225016));
#32601=CARTESIAN_POINT('Ctrl Pts',(6.10965004500316,1.125,14.75));
#32602=CARTESIAN_POINT('Ctrl Pts',(0.,1.2,14.75));
#32603=CARTESIAN_POINT('Ctrl Pts',(-6.10965004500315,1.275,14.75));
#32604=CARTESIAN_POINT('Ctrl Pts',(-10.4298250225016,1.35,10.4298250225016));
#32605=CARTESIAN_POINT('Ctrl Pts',(-14.75,1.425,6.10965004500315));
#32606=CARTESIAN_POINT('Ctrl Pts',(-14.75,1.5,9.03177014371173E-16));
#32607=CARTESIAN_POINT('Ctrl Pts',(-14.75,1.575,-6.10965004500315));
#32608=CARTESIAN_POINT('Ctrl Pts',(-10.4298250225016,1.65,-10.4298250225016));
#32609=CARTESIAN_POINT('Ctrl Pts',(-6.10965004500315,1.725,-14.75));
#32610=CARTESIAN_POINT('Ctrl Pts',(-1.80635402874235E-15,1.8,-14.75));
#32611=CARTESIAN_POINT('Ctrl Pts',(6.10965004500315,1.875,-14.75));
#32612=CARTESIAN_POINT('Ctrl Pts',(10.4298250225016,1.95,-10.4298250225016));
#32613=CARTESIAN_POINT('Ctrl Pts',(14.75,2.025,-6.10965004500316));
#32614=CARTESIAN_POINT('Ctrl Pts',(14.75,2.1,-2.70953104311352E-15));
#32615=CARTESIAN_POINT('Ctrl Pts',(14.75,2.17499999999999,6.10965004500316));
#32616=CARTESIAN_POINT('Ctrl Pts',(10.4298250225016,2.25,10.4298250225016));
#32617=CARTESIAN_POINT('Ctrl Pts',(6.10965004500316,2.32499999999999,14.75));
#32618=CARTESIAN_POINT('Ctrl Pts',(0.,2.39999999999999,14.75));
#32619=CARTESIAN_POINT('Ctrl Pts',(-6.10965004500315,2.47499999999999,14.75));
#32620=CARTESIAN_POINT('Ctrl Pts',(-10.4298250225016,2.54999999999999,10.4298250225016));
#32621=CARTESIAN_POINT('Ctrl Pts',(-14.75,2.62499999999999,6.10965004500315));
#32622=CARTESIAN_POINT('Ctrl Pts',(-14.75,2.69999999999999,9.03177014371173E-16));
#32623=CARTESIAN_POINT('Ctrl Pts',(-14.75,2.77499999999999,-6.10965004500315));
#32624=CARTESIAN_POINT('Ctrl Pts',(-10.4298250225016,2.84999999999999,-10.4298250225016));
#32625=CARTESIAN_POINT('Ctrl Pts',(-6.10965004500315,2.92499999999999,-14.75));
#32626=CARTESIAN_POINT('Ctrl Pts',(-1.80635402874235E-15,2.99999999999999,
-14.75));
#32627=CARTESIAN_POINT('Ctrl Pts',(6.10965004500315,3.07499999999999,-14.75));
#32628=CARTESIAN_POINT('Ctrl Pts',(10.4298250225016,3.14999999999999,-10.4298250225016));
#32629=CARTESIAN_POINT('Ctrl Pts',(14.75,3.22499999999999,-6.10965004500316));
#32630=CARTESIAN_POINT('Ctrl Pts',(14.75,3.29999999999999,-2.70953104311352E-15));
#32631=CARTESIAN_POINT('Ctrl Pts',(14.75,3.37499999999999,6.10965004500316));
#32632=CARTESIAN_POINT('Ctrl Pts',(10.4298250225016,3.44999999999999,10.4298250225016));
#32633=CARTESIAN_POINT('Ctrl Pts',(6.10965004500316,3.52499999999999,14.75));
#32634=CARTESIAN_POINT('Ctrl Pts',(0.,3.59999999999999,14.75));
#32635=CARTESIAN_POINT('Ctrl Pts',(-6.10965004500315,3.67499999999999,14.75));
#32636=CARTESIAN_POINT('Ctrl Pts',(-10.4298250225016,3.74999999999999,10.4298250225016));
#32637=CARTESIAN_POINT('Ctrl Pts',(-14.75,3.82499999999999,6.10965004500315));
#32638=CARTESIAN_POINT('Ctrl Pts',(-14.75,3.89999999999999,9.03177014371173E-16));
#32639=CARTESIAN_POINT('Ctrl Pts',(-14.75,3.97499999999999,-6.10965004500315));
#32640=CARTESIAN_POINT('Ctrl Pts',(-10.4298250225016,4.04999999999999,-10.4298250225016));
#32641=CARTESIAN_POINT('Ctrl Pts',(-6.10965004500315,4.12499999999999,-14.75));
#32642=CARTESIAN_POINT('Ctrl Pts',(-1.80635402874235E-15,4.19999999999999,
-14.75));
#32643=CARTESIAN_POINT('Ctrl Pts',(6.10965004500315,4.27499999999999,-14.75));
#32644=CARTESIAN_POINT('Ctrl Pts',(10.4298250225016,4.34999999999999,-10.4298250225016));
#32645=CARTESIAN_POINT('Ctrl Pts',(14.75,4.42499999999999,-6.10965004500316));
#32646=CARTESIAN_POINT('Ctrl Pts',(14.75,4.49999999999999,-2.70953104311352E-15));
#32647=CARTESIAN_POINT('Ctrl Pts',(14.75,4.57499999999999,6.10965004500316));
#32648=CARTESIAN_POINT('Ctrl Pts',(10.4298250225016,4.64999999999999,10.4298250225016));
#32649=CARTESIAN_POINT('Ctrl Pts',(6.10965004500316,4.72499999999999,14.75));
#32650=CARTESIAN_POINT('Ctrl Pts',(0.,4.79999999999999,14.75));
#32651=CARTESIAN_POINT('Origin',(0.,0.,14.15));
#32652=CARTESIAN_POINT('Origin',(-7.90471375114085E-13,4.8,14.15));
#32653=CARTESIAN_POINT('Origin',(-7.90471375114085E-13,4.8,14.15));
#32654=CARTESIAN_POINT('Origin',(0.,0.,14.15));
#32978=UNCERTAINTY_MEASURE_WITH_UNIT(LENGTH_MEASURE(0.01),#33017,
'DISTANCE_ACCURACY_VALUE',
'Maximum model space distance between geometric entities at asserted c
onnectivities');
#32984=UNCERTAINTY_MEASURE_WITH_UNIT(LENGTH_MEASURE(0.01),#33017,
'DISTANCE_ACCURACY_VALUE',
'Maximum model space distance between geometric entities at asserted c
onnectivities');
#33010=(
GEOMETRIC_REPRESENTATION_CONTEXT(3)
GLOBAL_UNCERTAINTY_ASSIGNED_CONTEXT((#32978))
GLOBAL_UNIT_ASSIGNED_CONTEXT((#33017,#33019,#33020))
REPRESENTATION_CONTEXT('','3D')
);
#33016=(
GEOMETRIC_REPRESENTATION_CONTEXT(3)
GLOBAL_UNCERTAINTY_ASSIGNED_CONTEXT((#32984))
GLOBAL_UNIT_ASSIGNED_CONTEXT((#33017,#33019,#33020))
REPRESENTATION_CONTEXT('','3D')
);
#33017=(
LENGTH_UNIT()
NAMED_UNIT(*)
SI_UNIT(.MILLI.,.METRE.)
);
#33019=(
NAMED_UNIT(*)
PLANE_ANGLE_UNIT()
SI_UNIT($,.RADIAN.)
);
#33020=(
NAMED_UNIT(*)
SI_UNIT($,.STERADIAN.)
SOLID_ANGLE_UNIT()
);
#33046=SHAPE_DEFINITION_REPRESENTATION(#33099,#33149);
#33099=PRODUCT_DEFINITION_SHAPE('',$,#33181);
#33149=SHAPE_REPRESENTATION('',(#11102),#33010);
#33155=PRODUCT_DEFINITION_CONTEXT('part definition',#33250,'design');
#33181=PRODUCT_DEFINITION(
'BO21-002_Spring_PUR-HW-4061_4T_1.2 mm x 29.5 mm x 28 mm (C)',
'PUR-HW-4061',#33212,#33155);
#33212=PRODUCT_DEFINITION_FORMATION('',$,#33277);
#33250=APPLICATION_CONTEXT(
'Core Data for Automotive Mechanical Design Process');
#33251=PRODUCT_CONTEXT('part definition',#33250,'mechanical');
#33277=PRODUCT(
'BO21-002_Spring_PUR-HW-4061_4T_1.2 mm x 29.5 mm x 28 mm (C)',
'PUR-HW-4061',$,(#33251));
#33285=PRESENTATION_STYLE_ASSIGNMENT((#33292));
#33292=SURFACE_STYLE_USAGE(.BOTH.,#33299);
#33299=SURFACE_SIDE_STYLE('',(#33306));
#33306=SURFACE_STYLE_FILL_AREA(#33313);
#33313=FILL_AREA_STYLE('Opaque(202,209,238)',(#33320));
#33320=FILL_AREA_STYLE_COLOUR('Opaque(202,209,238)',#33327);
#33327=COLOUR_RGB('Opaque(202,209,238)', 0.08235294, 0.09019608, 0.10196078);
ENDSEC;
END-ISO-10303-21;
